ISO-10303-21;
HEADER;
FILE_DESCRIPTION (('STEP AP214'),
    '1' );
FILE_NAME ('Pneumatic Toggle Clamp Unit.step',
    '2026-10-07T11:37:37',
    ( '' ),
    ( '' ),
    'SwSTEP 2.0',
    'SolidWorks 2020',
    '' );
FILE_SCHEMA (( 'AUTOMOTIVE_DESIGN' ));
ENDSEC;

DATA;
#75=CARTESIAN_POINT ( 'NONE',  ( -9.261585182541612227, 239.0000000000000000, 152.5407914452011369 ) ) ;
#87=EDGE_CURVE ( 'NONE', #55444, #20525, #67497, .T. ) ;
#130=CARTESIAN_POINT ( 'NONE',  ( 27.27158787008327678, 127.0000000000000000, 85.23828826961327820 ) ) ;
#198=EDGE_LOOP ( 'NONE', ( #58309, #71427, #79095, #45563, #21025 ) ) ;
#216=DIRECTION ( 'NONE',  ( -0.000000000000000000, 1.000000000000000000, -0.000000000000000000 ) ) ;
#259=CARTESIAN_POINT ( 'NONE',  ( 1.387778780781445676E-14, 224.4999999999999432, 97.27542076772557778 ) ) ;
#313=CARTESIAN_POINT ( 'NONE',  ( 0.000000000000000000, 184.0000000000000000, 101.0189074266571794 ) ) ;
#337=DIRECTION ( 'NONE',  ( 0.000000000000000000, 1.000000000000000000, 0.000000000000000000 ) ) ;
#352=ORIENTED_EDGE ( 'NONE', *, *, #65760, .T. ) ;
#361=EDGE_CURVE ( 'NONE', #26848, #11707, #28630, .T. ) ;
#408=DIRECTION ( 'NONE',  ( 0.000000000000000000, 0.000000000000000000, 1.000000000000000000 ) ) ;
#458=ORIENTED_EDGE ( 'NONE', *, *, #7648, .F. ) ;
#481=LINE ( 'NONE', #28173, #48342 ) ;
#643=CARTESIAN_POINT ( 'NONE',  ( 27.27158787008327678, 184.0000000000000000, 80.02307622376218887 ) ) ;
#729=CARTESIAN_POINT ( 'NONE',  ( -13.86911000615384104, 238.5000000000000000, 102.9892450244911828 ) ) ;
#738=AXIS2_PLACEMENT_3D ( 'NONE', #72305, #37331, #64151 ) ;
#779=EDGE_CURVE ( 'NONE', #44762, #23939, #63516, .T. ) ;
#1005=ORIENTED_EDGE ( 'NONE', *, *, #10407, .T. ) ;
#1043=ORIENTED_EDGE ( 'NONE', *, *, #73675, .T. ) ;
#1047=DIRECTION ( 'NONE',  ( 0.000000000000000000, -1.000000000000000000, 0.000000000000000000 ) ) ;
#1202=VERTEX_POINT ( 'NONE', #26225 ) ;
#1363=VERTEX_POINT ( 'NONE', #59288 ) ;
#1389=DIRECTION ( 'NONE',  ( -2.170915417798913418E-16, 0.000000000000000000, -1.000000000000000000 ) ) ;
#1397=ORIENTED_EDGE ( 'NONE', *, *, #20074, .T. ) ;
#1456=VECTOR ( 'NONE', #84613, 1000.000000000000000 ) ;
#1495=DIRECTION ( 'NONE',  ( -0.000000000000000000, 1.000000000000000000, -0.000000000000000000 ) ) ;
#1524=DIRECTION ( 'NONE',  ( 0.000000000000000000, 0.000000000000000000, -1.000000000000000000 ) ) ;
#1534=( GEOMETRIC_REPRESENTATION_CONTEXT ( 3 ) GLOBAL_UNCERTAINTY_ASSIGNED_CONTEXT ( ( #21509 ) ) GLOBAL_UNIT_ASSIGNED_CONTEXT ( ( #51859, #16479, #85981 ) ) REPRESENTATION_CONTEXT ( 'NONE', 'WORKASPACE' ) );
#1535=DIRECTION ( 'NONE',  ( 0.000000000000000000, 1.000000000000000000, 0.000000000000000000 ) ) ;
#1545=VERTEX_POINT ( 'NONE', #40641 ) ;
#1599=VERTEX_POINT ( 'NONE', #19312 ) ;
#1617=CARTESIAN_POINT ( 'NONE',  ( 1.224646799147354440E-15, 210.0000000000000000, 144.6557476874258441 ) ) ;
#1706=AXIS2_PLACEMENT_3D ( 'NONE', #3506, #72112, #31203 ) ;
#1823=CARTESIAN_POINT ( 'NONE',  ( 0.000000000000000000, 223.9999999999999716, 154.6557476874258441 ) ) ;
#1906=EDGE_CURVE ( 'NONE', #78790, #42810, #62296, .T. ) ;
#1917=CARTESIAN_POINT ( 'NONE',  ( 27.27158787008327678, 184.0000000000000000, 80.02307622376218887 ) ) ;
#1958=( NAMED_UNIT ( * ) PLANE_ANGLE_UNIT ( ) SI_UNIT ( $, .RADIAN. ) );
#1978=LINE ( 'NONE', #50556, #23345 ) ;
#2065=ORIENTED_EDGE ( 'NONE', *, *, #74567, .F. ) ;
#2093=EDGE_CURVE ( 'NONE', #43862, #24524, #11942, .T. ) ;
#2237=AXIS2_PLACEMENT_3D ( 'NONE', #1823, #57207, #23182 ) ;
#2388=AXIS2_PLACEMENT_3D ( 'NONE', #47422, #61503, #12935 ) ;
#2516=CARTESIAN_POINT ( 'NONE',  ( -24.79284581386642827, 184.0000000000000000, 0.000000000000000000 ) ) ;
#2539=PLANE ( 'NONE',  #66307 ) ;
#2575=ORIENTED_EDGE ( 'NONE', *, *, #75040, .T. ) ;
#2658=CARTESIAN_POINT ( 'NONE',  ( 27.27158787008325902, 184.0000000000000000, -5.920431057502157584E-15 ) ) ;
#2674=CARTESIAN_POINT ( 'NONE',  ( 0.000000000000000000, 184.0000000000000000, 101.0189074266571794 ) ) ;
#2716=CARTESIAN_POINT ( 'NONE',  ( 89.60916260784479448, 224.4999999999999432, 134.1927865330827103 ) ) ;
#2731=CARTESIAN_POINT ( 'NONE',  ( 1.387778780781445676E-14, 223.9999999999999716, 97.27542076772557778 ) ) ;
#2748=VECTOR ( 'NONE', #79612, 1000.000000000000000 ) ;
#2797=VERTEX_POINT ( 'NONE', #77876 ) ;
#2893=ADVANCED_FACE ( 'NONE', ( #24685 ), #11049, .F. ) ;
#2956=CARTESIAN_POINT ( 'NONE',  ( 1.387778780781445676E-14, 239.0000000000000000, 97.27542076772557778 ) ) ;
#3006=EDGE_CURVE ( 'NONE', #2797, #70996, #83842, .T. ) ;
#3024=DIRECTION ( 'NONE',  ( -2.170915417798913418E-16, 0.000000000000000000, -1.000000000000000000 ) ) ;
#3042=EDGE_CURVE ( 'NONE', #1363, #27566, #46445, .T. ) ;
#3176=LINE ( 'NONE', #30874, #50678 ) ;
#3192=DIRECTION ( 'NONE',  ( 0.000000000000000000, 1.000000000000000000, 0.000000000000000000 ) ) ;
#3257=EDGE_CURVE ( 'NONE', #21223, #28033, #72293, .T. ) ;
#3271=LINE ( 'NONE', #67262, #65315 ) ;
#3331=PRODUCT_DEFINITION ( 'UNKNOWN', '', #4369, #22642 ) ;
#3387=DIRECTION ( 'NONE',  ( 0.000000000000000000, 1.000000000000000000, 0.000000000000000000 ) ) ;
#3501=CARTESIAN_POINT ( 'NONE',  ( 24.79284581386629327, 127.0000000000000000, -3.384395586952189366E-14 ) ) ;
#3506=CARTESIAN_POINT ( 'NONE',  ( 27.27158787008325902, 184.0000000000000000, -5.920431057502157584E-15 ) ) ;
#3604=LINE ( 'NONE', #11766, #22319 ) ;
#3665=VECTOR ( 'NONE', #23121, 1000.000000000000000 ) ;
#3690=STYLED_ITEM ( 'NONE', ( #30873 ), #80543 ) ;
#3704=DIRECTION ( 'NONE',  ( -0.000000000000000000, 1.000000000000000000, -0.000000000000000000 ) ) ;
#3789=CARTESIAN_POINT ( 'NONE',  ( 1.387778780781445676E-14, 239.0000000000000000, 90.27542076772557778 ) ) ;
#3799=CIRCLE ( 'NONE', #87897, 5.000000000000004441 ) ;
#3943=ORIENTED_EDGE ( 'NONE', *, *, #75724, .F. ) ;
#3974=CIRCLE ( 'NONE', #15588, 7.199999999999998401 ) ;
#3999=DIRECTION ( 'NONE',  ( 0.000000000000000000, 0.000000000000000000, -1.000000000000000000 ) ) ;
#4082=ORIENTED_EDGE ( 'NONE', *, *, #12572, .F. ) ;
#4142=VERTEX_POINT ( 'NONE', #53933 ) ;
#4297=LINE ( 'NONE', #24735, #58623 ) ;
#4302=VECTOR ( 'NONE', #21212, 1000.000000000000000 ) ;
#4314=CARTESIAN_POINT ( 'NONE',  ( 27.27158787008328389, 184.0000000000000000, 106.1020876358972629 ) ) ;
#4369=PRODUCT_DEFINITION_FORMATION_WITH_SPECIFIED_SOURCE ( 'ANY', '', #38722, .NOT_KNOWN. ) ;
#4406=CYLINDRICAL_SURFACE ( 'NONE', #68755, 7.199999999999998401 ) ;
#4466=DIRECTION ( 'NONE',  ( -0.000000000000000000, -1.000000000000000000, 0.000000000000000000 ) ) ;
#4533=SHAPE_DEFINITION_REPRESENTATION ( #67029, #19449 ) ;
#4554=DIRECTION ( 'NONE',  ( -1.000000000000000000, 0.000000000000000000, 0.000000000000000000 ) ) ;
#4588=CARTESIAN_POINT ( 'NONE',  ( 24.79284581386643893, 184.0000000000000000, 106.1020876358972629 ) ) ;
#4670=ORIENTED_EDGE ( 'NONE', *, *, #13499, .F. ) ;
#4674=VECTOR ( 'NONE', #66600, 1000.000000000000000 ) ;
#4743=DIRECTION ( 'NONE',  ( 0.000000000000000000, 0.000000000000000000, 1.000000000000000000 ) ) ;
#4747=CARTESIAN_POINT ( 'NONE',  ( 0.000000000000000000, 223.9999999999999716, 164.1557476874258441 ) ) ;
#4860=CARTESIAN_POINT ( 'NONE',  ( 24.79284581386643893, 184.0000000000000000, 106.1020876358972629 ) ) ;
#4892=CARTESIAN_POINT ( 'NONE',  ( 1.387778780781445676E-14, 239.0000000000000000, 97.27542076772557778 ) ) ;
#4945=VECTOR ( 'NONE', #85269, 1000.000000000000000 ) ;
#4973=VERTEX_POINT ( 'NONE', #22287 ) ;
#5075=AXIS2_PLACEMENT_3D ( 'NONE', #89456, #62633, #408 ) ;
#5133=CARTESIAN_POINT ( 'NONE',  ( -27.27158787008326968, 184.0000000000000000, 85.23828826961327820 ) ) ;
#5158=ORIENTED_EDGE ( 'NONE', *, *, #87521, .T. ) ;
#5175=ORIENTED_EDGE ( 'NONE', *, *, #61362, .T. ) ;
#5184=AXIS2_PLACEMENT_3D ( 'NONE', #72080, #69958, #78903 ) ;
#5217=PLANE ( 'NONE',  #2388 ) ;
#5251=DIRECTION ( 'NONE',  ( 0.000000000000000000, 0.000000000000000000, -1.000000000000000000 ) ) ;
#5261=DIRECTION ( 'NONE',  ( -0.000000000000000000, -1.000000000000000000, -0.000000000000000000 ) ) ;
#5311=DIRECTION ( 'NONE',  ( 0.000000000000000000, 0.000000000000000000, 1.000000000000000000 ) ) ;
#5318=DIRECTION ( 'NONE',  ( 0.000000000000000000, 1.000000000000000000, 0.000000000000000000 ) ) ;
#5324=EDGE_LOOP ( 'NONE', ( #52472, #14426 ) ) ;
#5326=ORIENTED_EDGE ( 'NONE', *, *, #15556, .F. ) ;
#5354=DIRECTION ( 'NONE',  ( -0.000000000000000000, 1.000000000000000000, -0.000000000000000000 ) ) ;
#5509=VECTOR ( 'NONE', #48236, 1000.000000000000000 ) ;
#5642=DIRECTION ( 'NONE',  ( 1.000000000000000000, 0.000000000000000000, 0.000000000000000000 ) ) ;
#5740=CARTESIAN_POINT ( 'NONE',  ( -27.27158787008326968, 184.0000000000000000, 101.0189074266571794 ) ) ;
#5852=EDGE_CURVE ( 'NONE', #43862, #27454, #10391, .T. ) ;
#5869=ORIENTED_EDGE ( 'NONE', *, *, #17666, .T. ) ;
#6099=FACE_OUTER_BOUND ( 'NONE', #72737, .T. ) ;
#6100=CARTESIAN_POINT ( 'NONE',  ( -27.27158787008326968, 184.0000000000000000, 90.32146847885337593 ) ) ;
#6209=CARTESIAN_POINT ( 'NONE',  ( -89.60916260784479448, 238.5000000000000000, 134.1927865330827103 ) ) ;
#6243=DIRECTION ( 'NONE',  ( 0.000000000000000000, 1.000000000000000000, 0.000000000000000000 ) ) ;
#6245=DIRECTION ( 'NONE',  ( 0.000000000000000000, 1.000000000000000000, 0.000000000000000000 ) ) ;
#6585=FACE_OUTER_BOUND ( 'NONE', #46124, .T. ) ;
#6612=ADVANCED_FACE ( 'NONE', ( #41375 ), #71423, .F. ) ;
#6637=DIRECTION ( 'NONE',  ( 8.659560562355552854E-17, -0.7071067811864968355, 0.7071067811865981989 ) ) ;
#6644=CARTESIAN_POINT ( 'NONE',  ( 13.86911000615387302, 238.5000000000000000, 102.9892450244911686 ) ) ;
#6677=CARTESIAN_POINT ( 'NONE',  ( 24.79284581386643183, 127.0000000000000000, 101.0189074266571794 ) ) ;
#6813=VECTOR ( 'NONE', #58508, 1000.000000000000000 ) ;
#6825=ORIENTED_EDGE ( 'NONE', *, *, #20550, .F. ) ;
#6826=VERTEX_POINT ( 'NONE', #64973 ) ;
#6918=ORIENTED_EDGE ( 'NONE', *, *, #65156, .T. ) ;
#6924=CARTESIAN_POINT ( 'NONE',  ( 0.000000000000000000, 238.7999999999999829, 154.6557476874258441 ) ) ;
#6984=DIRECTION ( 'NONE',  ( 1.000000000000000000, 0.000000000000000000, 0.000000000000000000 ) ) ;
#6994=DIRECTION ( 'NONE',  ( -1.000000000000000000, -0.000000000000000000, -0.000000000000000000 ) ) ;
#7037=CARTESIAN_POINT ( 'NONE',  ( 0.000000000000000000, 210.0000000000000000, 154.6557476874258441 ) ) ;
#7327=LINE ( 'NONE', #83192, #12981 ) ;
#7398=ORIENTED_EDGE ( 'NONE', *, *, #74567, .T. ) ;
#7477=FACE_OUTER_BOUND ( 'NONE', #14553, .T. ) ;
#7546=DIRECTION ( 'NONE',  ( 0.000000000000000000, 0.000000000000000000, -1.000000000000000000 ) ) ;
#7648=EDGE_CURVE ( 'NONE', #83946, #1545, #1978, .T. ) ;
#7696=VECTOR ( 'NONE', #31389, 1000.000000000000000 ) ;
#7787=CARTESIAN_POINT ( 'NONE',  ( 0.000000000000000000, 211.0000000000000000, 154.6557476874258441 ) ) ;
#8041=EDGE_CURVE ( 'NONE', #82100, #70996, #35030, .T. ) ;
#8127=VECTOR ( 'NONE', #52781, 1000.000000000000000 ) ;
#8149=CIRCLE ( 'NONE', #85071, 9.500000000000008882 ) ;
#8270=ORIENTED_EDGE ( 'NONE', *, *, #31933, .F. ) ;
#8430=VECTOR ( 'NONE', #24139, 1000.000000000000000 ) ;
#8466=ORIENTED_EDGE ( 'NONE', *, *, #72556, .T. ) ;
#8473=CIRCLE ( 'NONE', #28750, 82.41591158490091118 ) ;
#8478=VECTOR ( 'NONE', #73106, 1000.000000000000000 ) ;
#8597=LINE ( 'NONE', #2674, #24265 ) ;
#8625=EDGE_CURVE ( 'NONE', #26264, #21297, #85350, .T. ) ;
#8802=STYLED_ITEM ( 'NONE', ( #50984 ), #28324 ) ;
#8803=CYLINDRICAL_SURFACE ( 'NONE', #21801, 7.199999999999998401 ) ;
#8838=ORIENTED_EDGE ( 'NONE', *, *, #15556, .T. ) ;
#8918=DIRECTION ( 'NONE',  ( 0.6537961156249325612, 0.7071067811865220376, -0.2693522585644785305 ) ) ;
#9008=ORIENTED_EDGE ( 'NONE', *, *, #77478, .T. ) ;
#9020=VERTEX_POINT ( 'NONE', #27008 ) ;
#9140=VERTEX_POINT ( 'NONE', #81103 ) ;
#9303=EDGE_CURVE ( 'NONE', #46763, #44762, #71927, .T. ) ;
#9524=DIRECTION ( 'NONE',  ( 0.000000000000000000, -1.000000000000000000, 0.000000000000000000 ) ) ;
#9554=EDGE_LOOP ( 'NONE', ( #88538, #53393, #38933, #6918 ) ) ;
#9657=LINE ( 'NONE', #58683, #2748 ) ;
#9693=ADVANCED_FACE ( 'NONE', ( #69577 ), #15065, .T. ) ;
#9734=DIRECTION ( 'NONE',  ( 0.000000000000000000, 1.000000000000000000, -0.000000000000000000 ) ) ;
#9753=EDGE_LOOP ( 'NONE', ( #85688, #83935 ) ) ;
#9774=LINE ( 'NONE', #80610, #29663 ) ;
#9777=DIRECTION ( 'NONE',  ( 0.000000000000000000, -0.000000000000000000, -1.000000000000000000 ) ) ;
#9789=FACE_OUTER_BOUND ( 'NONE', #38510, .T. ) ;
#9804=EDGE_LOOP ( 'NONE', ( #68646, #37684, #458, #48010 ) ) ;
#9816=EDGE_CURVE ( 'NONE', #58010, #15778, #29736, .T. ) ;
#9892=CONICAL_SURFACE ( 'NONE', #62073, 7.000000000000006217, 0.7853981633974699283 ) ;
#9968=ORIENTED_EDGE ( 'NONE', *, *, #52726, .T. ) ;
#9970=VECTOR ( 'NONE', #77127, 1000.000000000000000 ) ;
#10041=ORIENTED_EDGE ( 'NONE', *, *, #31933, .T. ) ;
#10074=EDGE_LOOP ( 'NONE', ( #48070, #72758, #3943, #72224 ) ) ;
#10082=DIRECTION ( 'NONE',  ( 0.000000000000000000, 0.000000000000000000, 1.000000000000000000 ) ) ;
#10090=VERTEX_POINT ( 'NONE', #50245 ) ;
#10093=FACE_OUTER_BOUND ( 'NONE', #9804, .T. ) ;
#10166=DIRECTION ( 'NONE',  ( 0.000000000000000000, -1.000000000000000000, 0.000000000000000000 ) ) ;
#10371=CARTESIAN_POINT ( 'NONE',  ( -27.27158787008326968, 127.0000000000000000, 101.0189074266571794 ) ) ;
#10391=CIRCLE ( 'NONE', #88729, 1.000000000000000888 ) ;
#10407=EDGE_CURVE ( 'NONE', #15778, #58010, #70657, .T. ) ;
#10444=CARTESIAN_POINT ( 'NONE',  ( 1.475953350320055108E-14, 223.9999999999999716, 90.07542076772557493 ) ) ;
#10457=DIRECTION ( 'NONE',  ( 0.000000000000000000, -1.000000000000000000, 0.000000000000000000 ) ) ;
#10520=ORIENTED_EDGE ( 'NONE', *, *, #31918, .F. ) ;
#10552=FACE_OUTER_BOUND ( 'NONE', #61752, .T. ) ;
#10613=DIRECTION ( 'NONE',  ( 0.000000000000000000, 0.000000000000000000, 1.000000000000000000 ) ) ;
#11041=CARTESIAN_POINT ( 'NONE',  ( 1.387778780781445676E-14, 239.0000000000000000, 90.07542076772557493 ) ) ;
#11049=PLANE ( 'NONE',  #42120 ) ;
#11152=LINE ( 'NONE', #52023, #89639 ) ;
#11193=VERTEX_POINT ( 'NONE', #85923 ) ;
#11230=CIRCLE ( 'NONE', #37304, 9.500000000000008882 ) ;
#11243=AXIS2_PLACEMENT_3D ( 'NONE', #14908, #57561, #42571 ) ;
#11309=DIRECTION ( 'NONE',  ( -2.170915417798913418E-16, 0.000000000000000000, -1.000000000000000000 ) ) ;
#11333=CARTESIAN_POINT ( 'NONE',  ( 1.163414459189986668E-15, 210.0000000000000000, 163.6557476874258441 ) ) ;
#11352=PLANE ( 'NONE',  #32017 ) ;
#11359=CARTESIAN_POINT ( 'NONE',  ( 0.000000000000000000, 184.0000000000000000, 90.32146847885337593 ) ) ;
#11383=LINE ( 'NONE', #40424, #60372 ) ;
#11417=ORIENTED_EDGE ( 'NONE', *, *, #20550, .T. ) ;
#11419=AXIS2_PLACEMENT_3D ( 'NONE', #21461, #20567, #48237 ) ;
#11525=CARTESIAN_POINT ( 'NONE',  ( -27.27158787008326968, 127.0000000000000000, 111.9860621927989826 ) ) ;
#11629=FACE_OUTER_BOUND ( 'NONE', #19887, .T. ) ;
#11637=LINE ( 'NONE', #52480, #79332 ) ;
#11654=LINE ( 'NONE', #5740, #4674 ) ;
#11707=VERTEX_POINT ( 'NONE', #32152 ) ;
#11745=ORIENTED_EDGE ( 'NONE', *, *, #84214, .T. ) ;
#11766=CARTESIAN_POINT ( 'NONE',  ( 27.27158787008325902, 127.0000000000000000, -5.920431057502157584E-15 ) ) ;
#11823=ORIENTED_EDGE ( 'NONE', *, *, #87471, .T. ) ;
#11840=ORIENTED_EDGE ( 'NONE', *, *, #23054, .T. ) ;
#11857=ORIENTED_EDGE ( 'NONE', *, *, #77098, .F. ) ;
#11907=CYLINDRICAL_SURFACE ( 'NONE', #27175, 5.000000000000004441 ) ;
#11942=LINE ( 'NONE', #75061, #75408 ) ;
#11950=CARTESIAN_POINT ( 'NONE',  ( 0.000000000000000000, 184.0000000000000000, 85.23828826961327820 ) ) ;
#12010=CARTESIAN_POINT ( 'NONE',  ( 9.261585182541617556, 239.0000000000000000, 152.5407914452011653 ) ) ;
#12035=CARTESIAN_POINT ( 'NONE',  ( -27.27158787008326968, 184.0000000000000000, 111.9860621927989826 ) ) ;
#12060=EDGE_CURVE ( 'NONE', #55007, #28894, #51593, .T. ) ;
#12071=ORIENTED_EDGE ( 'NONE', *, *, #9816, .F. ) ;
#12073=CARTESIAN_POINT ( 'NONE',  ( 1.387778780781445676E-14, 223.9999999999999716, 90.07542076772557493 ) ) ;
#12076=DIRECTION ( 'NONE',  ( 0.000000000000000000, 0.000000000000000000, 1.000000000000000000 ) ) ;
#12095=PLANE ( 'NONE',  #62523 ) ;
#12137=VERTEX_POINT ( 'NONE', #82807 ) ;
#12145=DIRECTION ( 'NONE',  ( 0.000000000000000000, -1.000000000000000000, 0.000000000000000000 ) ) ;
#12201=LINE ( 'NONE', #38552, #17629 ) ;
#12258=LINE ( 'NONE', #39953, #12418 ) ;
#12267=CARTESIAN_POINT ( 'NONE',  ( 27.27158787008327678, 184.0000000000000000, 101.0189074266571794 ) ) ;
#12364=EDGE_LOOP ( 'NONE', ( #70931, #84166, #13544, #37573 ) ) ;
#12410=CARTESIAN_POINT ( 'NONE',  ( -9.749037034254357081, 238.5000000000000000, 152.4294779587682456 ) ) ;
#12418=VECTOR ( 'NONE', #4554, 1000.000000000000000 ) ;
#12447=DIRECTION ( 'NONE',  ( 0.000000000000000000, -0.000000000000000000, 1.000000000000000000 ) ) ;
#12548=ORIENTED_EDGE ( 'NONE', *, *, #37517, .T. ) ;
#12572=EDGE_CURVE ( 'NONE', #28045, #55376, #59079, .T. ) ;
#12640=ADVANCED_FACE ( 'NONE', ( #53596 ), #40882, .F. ) ;
#12718=DIRECTION ( 'NONE',  ( 0.000000000000000000, 0.000000000000000000, 1.000000000000000000 ) ) ;
#12856=ORIENTED_EDGE ( 'NONE', *, *, #86441, .T. ) ;
#12881=EDGE_LOOP ( 'NONE', ( #59775, #24980, #5869, #15207 ) ) ;
#12896=ORIENTED_EDGE ( 'NONE', *, *, #62593, .T. ) ;
#12935=DIRECTION ( 'NONE',  ( 1.000000000000000000, 0.000000000000000000, -0.000000000000000000 ) ) ;
#12947=ORIENTED_EDGE ( 'NONE', *, *, #40397, .T. ) ;
#12981=VECTOR ( 'NONE', #20950, 1000.000000000000000 ) ;
#13003=CARTESIAN_POINT ( 'NONE',  ( 1.387778780781445676E-14, 239.0000000000000000, 97.27542076772557778 ) ) ;
#13028=ORIENTED_EDGE ( 'NONE', *, *, #779, .F. ) ;
#13045=CARTESIAN_POINT ( 'NONE',  ( -24.79284581386642827, 184.0000000000000000, 101.0189074266571794 ) ) ;
#13050=DIRECTION ( 'NONE',  ( 0.000000000000000000, 0.000000000000000000, 1.000000000000000000 ) ) ;
#13205=EDGE_CURVE ( 'NONE', #26848, #23939, #18283, .T. ) ;
#13226=FACE_BOUND ( 'NONE', #87368, .T. ) ;
#13348=CARTESIAN_POINT ( 'NONE',  ( 1.475953350320055108E-14, 239.0000000000000000, 104.4754207677255806 ) ) ;
#13351=FACE_BOUND ( 'NONE', #43356, .T. ) ;
#13455=CARTESIAN_POINT ( 'NONE',  ( 1.387778780781445676E-14, 239.0000000000000000, 97.27542076772557778 ) ) ;
#13499=EDGE_CURVE ( 'NONE', #22883, #76315, #68940, .T. ) ;
#13544=ORIENTED_EDGE ( 'NONE', *, *, #41461, .F. ) ;
#13555=LINE ( 'NONE', #69868, #39754 ) ;
#13588=EDGE_CURVE ( 'NONE', #15679, #21569, #88136, .T. ) ;
#13711=VECTOR ( 'NONE', #36949, 1000.000000000000000 ) ;
#13714=DIRECTION ( 'NONE',  ( 0.000000000000000000, 0.000000000000000000, 1.000000000000000000 ) ) ;
#13871=EDGE_LOOP ( 'NONE', ( #69010, #25676 ) ) ;
#13885=CARTESIAN_POINT ( 'NONE',  ( -9.749037034254357081, 224.4999999999999432, 152.4294779587682456 ) ) ;
#13901=CARTESIAN_POINT ( 'NONE',  ( 5.878304635907259698E-16, 239.0000000000000000, 159.4557476874258271 ) ) ;
#14107=EDGE_CURVE ( 'NONE', #41873, #2797, #18406, .T. ) ;
#14240=ORIENTED_EDGE ( 'NONE', *, *, #16071, .T. ) ;
#14278=CARTESIAN_POINT ( 'NONE',  ( 24.79284581386643183, 184.0000000000000000, 85.23828826961327820 ) ) ;
#14302=ORIENTED_EDGE ( 'NONE', *, *, #5852, .F. ) ;
#14310=EDGE_CURVE ( 'NONE', #27454, #17964, #63235, .T. ) ;
#14319=EDGE_CURVE ( 'NONE', #17076, #76315, #86914, .T. ) ;
#14355=ORIENTED_EDGE ( 'NONE', *, *, #48232, .F. ) ;
#14369=LINE ( 'NONE', #84317, #34090 ) ;
#14404=CARTESIAN_POINT ( 'NONE',  ( -89.60916260784479448, 223.9999999999999716, 134.1927865330827103 ) ) ;
#14426=ORIENTED_EDGE ( 'NONE', *, *, #23054, .F. ) ;
#14438=DIRECTION ( 'NONE',  ( 0.000000000000000000, -0.7071067811864968355, -0.7071067811865981989 ) ) ;
#14452=CARTESIAN_POINT ( 'NONE',  ( 24.79284581386643183, 184.0000000000000000, 101.0189074266571794 ) ) ;
#14505=ADVANCED_FACE ( 'NONE', ( #40537 ), #26467, .F. ) ;
#14524=EDGE_CURVE ( 'NONE', #55444, #67055, #32825, .T. ) ;
#14535=DIRECTION ( 'NONE',  ( 0.000000000000000000, -1.000000000000000000, 0.000000000000000000 ) ) ;
#14553=EDGE_LOOP ( 'NONE', ( #22669, #38238, #34357, #26263 ) ) ;
#14617=ORIENTED_EDGE ( 'NONE', *, *, #48232, .T. ) ;
#14672=VERTEX_POINT ( 'NONE', #82798 ) ;
#14908=CARTESIAN_POINT ( 'NONE',  ( 89.60916260784479448, 238.5000000000000000, 134.1927865330827103 ) ) ;
#14933=EDGE_LOOP ( 'NONE', ( #56234, #50532 ) ) ;
#15065=PLANE ( 'NONE',  #45643 ) ;
#15070=VERTEX_POINT ( 'NONE', #82240 ) ;
#15084=VERTEX_POINT ( 'NONE', #83570 ) ;
#15089=CARTESIAN_POINT ( 'NONE',  ( -27.27158787008326968, 184.0000000000000000, 80.02307622376218887 ) ) ;
#15104=CARTESIAN_POINT ( 'NONE',  ( 0.000000000000000000, 127.0000000000000000, 85.23828826961327820 ) ) ;
#15106=LINE ( 'NONE', #85517, #69743 ) ;
#15207=ORIENTED_EDGE ( 'NONE', *, *, #46643, .T. ) ;
#15259=CARTESIAN_POINT ( 'NONE',  ( -24.79284581386642827, 127.0000000000000000, 106.1020876358972771 ) ) ;
#15273=DIRECTION ( 'NONE',  ( -0.000000000000000000, 1.000000000000000000, -0.000000000000000000 ) ) ;
#15457=CARTESIAN_POINT ( 'NONE',  ( 0.000000000000000000, 215.0000000000000000, 154.6557476874258441 ) ) ;
#15556=EDGE_CURVE ( 'NONE', #21297, #73197, #43444, .T. ) ;
#15588=AXIS2_PLACEMENT_3D ( 'NONE', #23228, #65854, #24100 ) ;
#15673=ADVANCED_FACE ( 'NONE', ( #11629 ), #52536, .F. ) ;
#15679=VERTEX_POINT ( 'NONE', #73391 ) ;
#15739=CARTESIAN_POINT ( 'NONE',  ( 13.86911000615387302, 238.5000000000000000, 102.9892450244911686 ) ) ;
#15778=VERTEX_POINT ( 'NONE', #12073 ) ;
#15845=ADVANCED_FACE ( 'NONE', ( #35980 ), #30788, .T. ) ;
#15854=LINE ( 'NONE', #23577, #6813 ) ;
#15869=AXIS2_PLACEMENT_3D ( 'NONE', #68635, #54965, #41350 ) ;
#15896=DIRECTION ( 'NONE',  ( 0.000000000000000000, -1.000000000000000000, 0.000000000000000000 ) ) ;
#15911=AXIS2_PLACEMENT_3D ( 'NONE', #43793, #9734, #10613 ) ;
#15922=ORIENTED_EDGE ( 'NONE', *, *, #38302, .F. ) ;
#15992=AXIS2_PLACEMENT_3D ( 'NONE', #74453, #79947, #45382 ) ;
#16049=FACE_OUTER_BOUND ( 'NONE', #54944, .T. ) ;
#16071=EDGE_CURVE ( 'NONE', #48691, #73197, #44565, .T. ) ;
#16073=DIRECTION ( 'NONE',  ( 0.000000000000000000, 0.000000000000000000, -1.000000000000000000 ) ) ;
#16115=FACE_OUTER_BOUND ( 'NONE', #31716, .T. ) ;
#16156=CARTESIAN_POINT ( 'NONE',  ( 0.000000000000000000, 215.0000000000000000, 154.6557476874258441 ) ) ;
#16186=EDGE_CURVE ( 'NONE', #25689, #28894, #30069, .T. ) ;
#16443=CARTESIAN_POINT ( 'NONE',  ( -24.79284581386642827, 127.0000000000000000, 90.32146847885337593 ) ) ;
#16479=( NAMED_UNIT ( * ) PLANE_ANGLE_UNIT ( ) SI_UNIT ( $, .RADIAN. ) );
#16487=PLANE ( 'NONE',  #27815 ) ;
#16640=AXIS2_PLACEMENT_3D ( 'NONE', #86866, #45490, #71901 ) ;
#16646=DIRECTION ( 'NONE',  ( 0.000000000000000000, 0.000000000000000000, 1.000000000000000000 ) ) ;
#16802=SURFACE_STYLE_FILL_AREA ( #58127 ) ;
#16881=AXIS2_PLACEMENT_3D ( 'NONE', #11950, #39635, #26024 ) ;
#16926=UNCERTAINTY_MEASURE_WITH_UNIT (LENGTH_MEASURE( 1.000000000000000082E-05 ), #37244, 'distance_accuracy_value', 'NONE');
#17076=VERTEX_POINT ( 'NONE', #53024 ) ;
#17081=CARTESIAN_POINT ( 'NONE',  ( 24.79284581386643893, 127.0000000000000000, 106.1020876358972629 ) ) ;
#17166=CARTESIAN_POINT ( 'NONE',  ( 0.000000000000000000, 223.9999999999999716, 154.6557476874258441 ) ) ;
#17231=EDGE_LOOP ( 'NONE', ( #87583, #28167, #87644, #11857 ) ) ;
#17354=VECTOR ( 'NONE', #17584, 1000.000000000000000 ) ;
#17584=DIRECTION ( 'NONE',  ( 0.000000000000000000, 0.000000000000000000, 1.000000000000000000 ) ) ;
#17628=ORIENTED_EDGE ( 'NONE', *, *, #1906, .F. ) ;
#17629=VECTOR ( 'NONE', #53040, 1000.000000000000000 ) ;
#17649=ORIENTED_EDGE ( 'NONE', *, *, #83046, .T. ) ;
#17666=EDGE_CURVE ( 'NONE', #26264, #54446, #22824, .T. ) ;
#17701=DIRECTION ( 'NONE',  ( 0.000000000000000000, 0.000000000000000000, -1.000000000000000000 ) ) ;
#17737=AXIS2_PLACEMENT_3D ( 'NONE', #30361, #85786, #23560 ) ;
#17781=FACE_OUTER_BOUND ( 'NONE', #34322, .T. ) ;
#17789=CARTESIAN_POINT ( 'NONE',  ( -27.27158787008326968, 184.0000000000000000, 90.32146847885337593 ) ) ;
#17887=CONICAL_SURFACE ( 'NONE', #83206, 15.00000000000000000, 0.7853981633974691512 ) ;
#17964=VERTEX_POINT ( 'NONE', #62690 ) ;
#18039=DIRECTION ( 'NONE',  ( 0.000000000000000000, 0.000000000000000000, 1.000000000000000000 ) ) ;
#18188=EDGE_CURVE ( 'NONE', #27566, #1599, #12201, .T. ) ;
#18196=EDGE_LOOP ( 'NONE', ( #53323, #40352, #78466, #56754 ) ) ;
#18228=ORIENTED_EDGE ( 'NONE', *, *, #39298, .T. ) ;
#18283=LINE ( 'NONE', #19194, #86329 ) ;
#18295=DIRECTION ( 'NONE',  ( -0.000000000000000000, 1.000000000000000000, -0.000000000000000000 ) ) ;
#18331=ORIENTED_EDGE ( 'NONE', *, *, #2093, .F. ) ;
#18342=CARTESIAN_POINT ( 'NONE',  ( -9.749037034254357081, 223.9999999999999716, 152.4294779587682456 ) ) ;
#18380=VECTOR ( 'NONE', #32083, 1000.000000000000000 ) ;
#18385=FACE_OUTER_BOUND ( 'NONE', #53887, .T. ) ;
#18406=LINE ( 'NONE', #52887, #57454 ) ;
#18518=PLANE ( 'NONE',  #89317 ) ;
#18594=AXIS2_PLACEMENT_3D ( 'NONE', #31937, #10166, #87366 ) ;
#18674=VECTOR ( 'NONE', #24734, 1000.000000000000000 ) ;
#18692=ORIENTED_EDGE ( 'NONE', *, *, #71780, .T. ) ;
#18843=AXIS2_PLACEMENT_3D ( 'NONE', #2956, #31538, #59241 ) ;
#18904=DIRECTION ( 'NONE',  ( -1.000000000000000000, 0.000000000000000000, -0.000000000000000000 ) ) ;
#18972=DIRECTION ( 'NONE',  ( 0.000000000000000000, 0.000000000000000000, 1.000000000000000000 ) ) ;
#18979=ADVANCED_FACE ( 'NONE', ( #60914 ), #86513, .T. ) ;
#19036=LINE ( 'NONE', #80388, #49356 ) ;
#19040=CARTESIAN_POINT ( 'NONE',  ( 9.749037034254362410, 223.9999999999999716, 152.4294779587682740 ) ) ;
#19053=FACE_OUTER_BOUND ( 'NONE', #62649, .T. ) ;
#19139=ADVANCED_FACE ( 'NONE', ( #42251, #77245, #13226 ), #89080, .T. ) ;
#19144=ORIENTED_EDGE ( 'NONE', *, *, #37020, .F. ) ;
#19194=CARTESIAN_POINT ( 'NONE',  ( 13.86911000615387302, 223.9999999999999716, 102.9892450244911686 ) ) ;
#19265=DIRECTION ( 'NONE',  ( 0.000000000000000000, 0.000000000000000000, 1.000000000000000000 ) ) ;
#19269=DIRECTION ( 'NONE',  ( 0.6893610196960192615, -0.7071067811865284769, -0.1574210421884302824 ) ) ;
#19312=CARTESIAN_POINT ( 'NONE',  ( -27.27158787008326968, 127.0000000000000000, 80.02307622376218887 ) ) ;
#19322=DIRECTION ( 'NONE',  ( 0.000000000000000000, -0.000000000000000000, 1.000000000000000000 ) ) ;
#19324=EDGE_CURVE ( 'NONE', #26264, #48691, #3176, .T. ) ;
#19409=ORIENTED_EDGE ( 'NONE', *, *, #21492, .F. ) ;
#19449=SHAPE_REPRESENTATION ( 'Pneumatic Toggle Clamp Unit', ( #50656 ), #23133 ) ;
#19506=AXIS2_PLACEMENT_3D ( 'NONE', #66481, #60556, #32399 ) ;
#19519=CARTESIAN_POINT ( 'NONE',  ( -27.27158787008326968, 184.0000000000000000, 0.000000000000000000 ) ) ;
#19607=CARTESIAN_POINT ( 'NONE',  ( 0.000000000000000000, 215.0000000000000000, 154.6557476874258441 ) ) ;
#19887=EDGE_LOOP ( 'NONE', ( #48358, #62696, #17649, #63253 ) ) ;
#19912=CARTESIAN_POINT ( 'NONE',  ( 1.387778780781445676E-14, 238.8000000000000114, 104.4754207677255806 ) ) ;
#19947=CIRCLE ( 'NONE', #11243, 81.91591158490091118 ) ;
#20013=ORIENTED_EDGE ( 'NONE', *, *, #64808, .T. ) ;
#20074=EDGE_CURVE ( 'NONE', #79794, #71248, #79829, .T. ) ;
#20123=ADVANCED_FACE ( 'NONE', ( #27964 ), #69763, .T. ) ;
#20125=ORIENTED_EDGE ( 'NONE', *, *, #37660, .F. ) ;
#20168=FACE_OUTER_BOUND ( 'NONE', #81385, .T. ) ;
#20267=ORIENTED_EDGE ( 'NONE', *, *, #22458, .F. ) ;
#20326=DIRECTION ( 'NONE',  ( 0.000000000000000000, 0.000000000000000000, 1.000000000000000000 ) ) ;
#20336=CONICAL_SURFACE ( 'NONE', #59469, 14.49999999999997158, 0.7853981633974743692 ) ;
#20445=DIRECTION ( 'NONE',  ( -0.000000000000000000, -1.000000000000000000, -0.000000000000000000 ) ) ;
#20460=DIRECTION ( 'NONE',  ( 0.000000000000000000, -0.000000000000000000, 1.000000000000000000 ) ) ;
#20487=ADVANCED_FACE ( 'NONE', ( #66052 ), #26107, .T. ) ;
#20525=VERTEX_POINT ( 'NONE', #48278 ) ;
#20550=EDGE_CURVE ( 'NONE', #58010, #63589, #48726, .T. ) ;
#20567=DIRECTION ( 'NONE',  ( -0.000000000000000000, 1.000000000000000000, -0.000000000000000000 ) ) ;
#20578=CARTESIAN_POINT ( 'NONE',  ( 0.000000000000000000, 223.9999999999999716, 159.6557476874258441 ) ) ;
#20585=EDGE_CURVE ( 'NONE', #11707, #45346, #26520, .T. ) ;
#20602=AXIS2_PLACEMENT_3D ( 'NONE', #86954, #3387, #72866 ) ;
#20610=DIRECTION ( 'NONE',  ( 0.000000000000000000, 1.000000000000000000, 0.000000000000000000 ) ) ;
#20689=EDGE_LOOP ( 'NONE', ( #61137, #54078, #56247, #31840 ) ) ;
#20714=DIRECTION ( 'NONE',  ( 0.000000000000000000, 0.000000000000000000, 1.000000000000000000 ) ) ;
#20723=AXIS2_PLACEMENT_3D ( 'NONE', #31021, #37847, #16073 ) ;
#20776=VECTOR ( 'NONE', #84097, 1000.000000000000000 ) ;
#20810=LINE ( 'NONE', #35768, #59763 ) ;
#20839=LINE ( 'NONE', #27202, #86626 ) ;
#20841=EDGE_LOOP ( 'NONE', ( #6825, #49452, #36267, #32628 ) ) ;
#20862=CARTESIAN_POINT ( 'NONE',  ( 2.849336855536075284E-14, 127.0000000000000000, 111.9860621927989683 ) ) ;
#20863=EDGE_CURVE ( 'NONE', #9020, #63589, #26163, .T. ) ;
#20950=DIRECTION ( 'NONE',  ( -0.000000000000000000, -1.000000000000000000, -0.000000000000000000 ) ) ;
#20970=ORIENTED_EDGE ( 'NONE', *, *, #17666, .F. ) ;
#21025=ORIENTED_EDGE ( 'NONE', *, *, #67620, .T. ) ;
#21160=VECTOR ( 'NONE', #25899, 1000.000000000000000 ) ;
#21212=DIRECTION ( 'NONE',  ( -1.000000000000000000, 0.000000000000000000, 0.000000000000000000 ) ) ;
#21223=VERTEX_POINT ( 'NONE', #11525 ) ;
#21297=VERTEX_POINT ( 'NONE', #130 ) ;
#21320=CARTESIAN_POINT ( 'NONE',  ( -9.749037034254353529, 224.4999999999999432, 152.4294779587682456 ) ) ;
#21461=CARTESIAN_POINT ( 'NONE',  ( 0.000000000000000000, 224.4999999999999432, 154.6557476874258441 ) ) ;
#21492=EDGE_CURVE ( 'NONE', #28894, #71248, #15106, .T. ) ;
#21509=UNCERTAINTY_MEASURE_WITH_UNIT (LENGTH_MEASURE( 1.000000000000000082E-05 ), #51859, 'distance_accuracy_value', 'NONE');
#21569=VERTEX_POINT ( 'NONE', #43238 ) ;
#21618=DIRECTION ( 'NONE',  ( -0.000000000000000000, 1.000000000000000000, -0.000000000000000000 ) ) ;
#21634=DIRECTION ( 'NONE',  ( 0.000000000000000000, 1.000000000000000000, 0.000000000000000000 ) ) ;
#21647=AXIS2_PLACEMENT_3D ( 'NONE', #54761, #82530, #5311 ) ;
#21666=AXIS2_PLACEMENT_3D ( 'NONE', #56953, #84246, #76968 ) ;
#21716=CARTESIAN_POINT ( 'NONE',  ( 27.27158787008327678, 127.0000000000000000, 80.02307622376218887 ) ) ;
#21801=AXIS2_PLACEMENT_3D ( 'NONE', #41938, #1535, #49202 ) ;
#21817=ORIENTED_EDGE ( 'NONE', *, *, #71496, .T. ) ;
#22007=VECTOR ( 'NONE', #26535, 1000.000000000000000 ) ;
#22014=EDGE_CURVE ( 'NONE', #42594, #79965, #79031, .T. ) ;
#22119=EDGE_LOOP ( 'NONE', ( #46810, #14355, #58523, #39866 ) ) ;
#22227=DIRECTION ( 'NONE',  ( 1.000000000000000000, -0.000000000000000000, 0.000000000000000000 ) ) ;
#22254=DIRECTION ( 'NONE',  ( -0.000000000000000000, -1.000000000000000000, 0.000000000000000000 ) ) ;
#22287=CARTESIAN_POINT ( 'NONE',  ( -24.79284581386642827, 184.0000000000000000, 106.1020876358972771 ) ) ;
#22319=VECTOR ( 'NONE', #11309, 1000.000000000000000 ) ;
#22320=DIRECTION ( 'NONE',  ( -0.000000000000000000, 1.000000000000000000, -0.000000000000000000 ) ) ;
#22393=CARTESIAN_POINT ( 'NONE',  ( 0.000000000000000000, 210.0000000000000000, 154.6557476874258441 ) ) ;
#22403=( LENGTH_UNIT ( ) NAMED_UNIT ( * ) SI_UNIT ( .MILLI., .METRE. ) );
#22458=EDGE_CURVE ( 'NONE', #46976, #12137, #84844, .T. ) ;
#22520=CARTESIAN_POINT ( 'NONE',  ( 1.102182119232618897E-15, 211.0000000000000000, 163.6557476874258441 ) ) ;
#22642=PRODUCT_DEFINITION_CONTEXT ( 'detailed design', #32907, 'design' ) ;
#22669=ORIENTED_EDGE ( 'NONE', *, *, #56134, .T. ) ;
#22766=EDGE_CURVE ( 'NONE', #54446, #67055, #83273, .T. ) ;
#22824=LINE ( 'NONE', #85057, #88829 ) ;
#22847=CARTESIAN_POINT ( 'NONE',  ( 13.86911000615387302, 224.4999999999999432, 102.9892450244911686 ) ) ;
#22849=CARTESIAN_POINT ( 'NONE',  ( 1.475953350320055108E-14, 184.0000000000000000, 104.4754207677255806 ) ) ;
#22883=VERTEX_POINT ( 'NONE', #64610 ) ;
#22941=ORIENTED_EDGE ( 'NONE', *, *, #13205, .F. ) ;
#23054=EDGE_CURVE ( 'NONE', #15084, #38527, #44077, .T. ) ;
#23055=CONICAL_SURFACE ( 'NONE', #11419, 10.00000000000000888, 0.7853981633974691512 ) ;
#23108=CONICAL_SURFACE ( 'NONE', #21666, 82.41591158490093960, 0.7853981633974760346 ) ;
#23121=DIRECTION ( 'NONE',  ( -0.000000000000000000, -1.000000000000000000, -0.000000000000000000 ) ) ;
#23131=CIRCLE ( 'NONE', #73859, 81.91591158490091118 ) ;
#23133=( GEOMETRIC_REPRESENTATION_CONTEXT ( 3 ) GLOBAL_UNCERTAINTY_ASSIGNED_CONTEXT ( ( #53528 ) ) GLOBAL_UNIT_ASSIGNED_CONTEXT ( ( #22403, #1958, #71007 ) ) REPRESENTATION_CONTEXT ( 'NONE', 'WORKASPACE' ) );
#23182=DIRECTION ( 'NONE',  ( 0.000000000000000000, 0.000000000000000000, 1.000000000000000000 ) ) ;
#23228=CARTESIAN_POINT ( 'NONE',  ( 1.387778780781445676E-14, 239.0000000000000000, 97.27542076772557778 ) ) ;
#23345=VECTOR ( 'NONE', #34689, 1000.000000000000114 ) ;
#23560=DIRECTION ( 'NONE',  ( 0.000000000000000000, 0.000000000000000000, -1.000000000000000000 ) ) ;
#23577=CARTESIAN_POINT ( 'NONE',  ( 0.000000000000000000, 127.0000000000000000, 85.23828826961327820 ) ) ;
#23645=ORIENTED_EDGE ( 'NONE', *, *, #38302, .T. ) ;
#23679=CARTESIAN_POINT ( 'NONE',  ( 1.387778780781445676E-14, 239.0000000000000000, 104.4754207677255806 ) ) ;
#23857=DIRECTION ( 'NONE',  ( -1.000000000000000000, 0.000000000000000000, 0.000000000000000000 ) ) ;
#23939=VERTEX_POINT ( 'NONE', #6644 ) ;
#23989=EDGE_LOOP ( 'NONE', ( #87441, #80978, #8466, #35575 ) ) ;
#23992=DIRECTION ( 'NONE',  ( 0.000000000000000000, 0.000000000000000000, 1.000000000000000000 ) ) ;
#24029=ORIENTED_EDGE ( 'NONE', *, *, #20585, .T. ) ;
#24067=DIRECTION ( 'NONE',  ( -0.000000000000000000, -1.000000000000000000, 0.000000000000000000 ) ) ;
#24100=DIRECTION ( 'NONE',  ( 0.000000000000000000, 0.000000000000000000, 1.000000000000000000 ) ) ;
#24133=ORIENTED_EDGE ( 'NONE', *, *, #19324, .T. ) ;
#24139=DIRECTION ( 'NONE',  ( 0.000000000000000000, 0.000000000000000000, -1.000000000000000000 ) ) ;
#24152=EDGE_CURVE ( 'NONE', #1363, #1202, #14369, .T. ) ;
#24253=ORIENTED_EDGE ( 'NONE', *, *, #55152, .F. ) ;
#24265=VECTOR ( 'NONE', #22227, 1000.000000000000000 ) ;
#24291=AXIS2_PLACEMENT_3D ( 'NONE', #259, #21618, #35669 ) ;
#24332=AXIS2_PLACEMENT_3D ( 'NONE', #36898, #1495, #64607 ) ;
#24411=FACE_OUTER_BOUND ( 'NONE', #75554, .T. ) ;
#24435=FACE_OUTER_BOUND ( 'NONE', #49727, .T. ) ;
#24505=CARTESIAN_POINT ( 'NONE',  ( 27.27158787008327678, 184.0000000000000000, 85.23828826961327820 ) ) ;
#24511=CARTESIAN_POINT ( 'NONE',  ( 1.387778780781445676E-14, 239.0000000000000000, 97.27542076772557778 ) ) ;
#24522=LINE ( 'NONE', #19040, #8478 ) ;
#24524=VERTEX_POINT ( 'NONE', #67403 ) ;
#24623=ORIENTED_EDGE ( 'NONE', *, *, #44244, .F. ) ;
#24643=ADVANCED_FACE ( 'NONE', ( #16049 ), #45742, .T. ) ;
#24685=FACE_OUTER_BOUND ( 'NONE', #87198, .T. ) ;
#24731=DIRECTION ( 'NONE',  ( 0.000000000000000000, -1.000000000000000000, 0.000000000000000000 ) ) ;
#24734=DIRECTION ( 'NONE',  ( -1.000000000000000000, 0.000000000000000000, 2.544367396927093851E-16 ) ) ;
#24735=CARTESIAN_POINT ( 'NONE',  ( 0.000000000000000000, 184.0000000000000000, 106.1020876358972629 ) ) ;
#24782=DIRECTION ( 'NONE',  ( 0.000000000000000000, 0.000000000000000000, 1.000000000000000000 ) ) ;
#24879=EDGE_CURVE ( 'NONE', #69728, #2797, #82111, .T. ) ;
#24980=ORIENTED_EDGE ( 'NONE', *, *, #8625, .F. ) ;
#25047=EDGE_CURVE ( 'NONE', #63589, #9020, #54493, .T. ) ;
#25201=DIRECTION ( 'NONE',  ( -0.000000000000000000, -1.000000000000000000, 0.000000000000000000 ) ) ;
#25202=ORIENTED_EDGE ( 'NONE', *, *, #83386, .T. ) ;
#25253=ADVANCED_FACE ( 'NONE', ( #38778 ), #53277, .T. ) ;
#25506=DIRECTION ( 'NONE',  ( 0.000000000000000000, 1.000000000000000000, 0.000000000000000000 ) ) ;
#25613=VECTOR ( 'NONE', #14438, 1000.000000000000114 ) ;
#25676=ORIENTED_EDGE ( 'NONE', *, *, #78415, .T. ) ;
#25689=VERTEX_POINT ( 'NONE', #17789 ) ;
#25717=FACE_OUTER_BOUND ( 'NONE', #34500, .T. ) ;
#25859=LINE ( 'NONE', #10444, #36012 ) ;
#25899=DIRECTION ( 'NONE',  ( -0.000000000000000000, -1.000000000000000000, -0.000000000000000000 ) ) ;
#25920=EDGE_CURVE ( 'NONE', #21569, #48100, #481, .T. ) ;
#26024=DIRECTION ( 'NONE',  ( -1.000000000000000000, 0.000000000000000000, -0.000000000000000000 ) ) ;
#26107=CONICAL_SURFACE ( 'NONE', #18843, 7.000000000000006217, 0.7853981633974699283 ) ;
#26163=CIRCLE ( 'NONE', #87124, 7.199999999999998401 ) ;
#26214=EDGE_CURVE ( 'NONE', #21569, #20525, #3604, .T. ) ;
#26225=CARTESIAN_POINT ( 'NONE',  ( -27.27158787008326968, 184.0000000000000000, 80.02307622376218887 ) ) ;
#26239=DIRECTION ( 'NONE',  ( 0.000000000000000000, 0.000000000000000000, 1.000000000000000000 ) ) ;
#26263=ORIENTED_EDGE ( 'NONE', *, *, #44664, .F. ) ;
#26264=VERTEX_POINT ( 'NONE', #24505 ) ;
#26354=ORIENTED_EDGE ( 'NONE', *, *, #84214, .F. ) ;
#26388=EDGE_LOOP ( 'NONE', ( #33416, #84896 ) ) ;
#26391=CIRCLE ( 'NONE', #35134, 14.49999999999997158 ) ;
#26407=DIRECTION ( 'NONE',  ( 0.000000000000000000, 0.000000000000000000, 1.000000000000000000 ) ) ;
#26467=PLANE ( 'NONE',  #16881 ) ;
#26520=LINE ( 'NONE', #27856, #47867 ) ;
#26535=DIRECTION ( 'NONE',  ( -0.000000000000000000, 1.000000000000000000, -0.000000000000000000 ) ) ;
#26737=VECTOR ( 'NONE', #78830, 1000.000000000000000 ) ;
#26848=VERTEX_POINT ( 'NONE', #22847 ) ;
#26999=VECTOR ( 'NONE', #66898, 1000.000000000000000 ) ;
#27008=CARTESIAN_POINT ( 'NONE',  ( 1.387778780781445676E-14, 184.0000000000000000, 90.07542076772557493 ) ) ;
#27139=CARTESIAN_POINT ( 'NONE',  ( 0.000000000000000000, 223.9999999999999716, 154.6557476874258441 ) ) ;
#27157=CARTESIAN_POINT ( 'NONE',  ( 0.000000000000000000, 239.0000000000000000, 149.8557476874258896 ) ) ;
#27175=AXIS2_PLACEMENT_3D ( 'NONE', #19607, #54098, #27316 ) ;
#27202=CARTESIAN_POINT ( 'NONE',  ( -24.79284581386642827, 184.0000000000000000, 106.1020876358972771 ) ) ;
#27316=DIRECTION ( 'NONE',  ( 0.000000000000000000, 0.000000000000000000, 1.000000000000000000 ) ) ;
#27317=CIRCLE ( 'NONE', #31661, 10.00000000000000888 ) ;
#27396=CARTESIAN_POINT ( 'NONE',  ( 24.79284581386643183, 184.0000000000000000, 0.000000000000000000 ) ) ;
#27454=VERTEX_POINT ( 'NONE', #11333 ) ;
#27508=DIRECTION ( 'NONE',  ( 0.000000000000000000, 0.000000000000000000, 1.000000000000000000 ) ) ;
#27564=CARTESIAN_POINT ( 'NONE',  ( -89.60916260784479448, 239.0000000000000000, 134.1927865330827103 ) ) ;
#27566=VERTEX_POINT ( 'NONE', #39485 ) ;
#27653=ORIENTED_EDGE ( 'NONE', *, *, #57080, .T. ) ;
#27765=EDGE_CURVE ( 'NONE', #4142, #11193, #59567, .T. ) ;
#27767=FACE_OUTER_BOUND ( 'NONE', #88464, .T. ) ;
#27798=ADVANCED_FACE ( 'NONE', ( #36712 ), #30343, .T. ) ;
#27815=AXIS2_PLACEMENT_3D ( 'NONE', #45492, #44164, #57354 ) ;
#27848=DIRECTION ( 'NONE',  ( 0.000000000000000000, -0.000000000000000000, -1.000000000000000000 ) ) ;
#27856=CARTESIAN_POINT ( 'NONE',  ( -13.86911000615384104, 223.9999999999999716, 102.9892450244911828 ) ) ;
#27861=DIRECTION ( 'NONE',  ( 0.000000000000000000, 0.000000000000000000, 1.000000000000000000 ) ) ;
#27894=AXIS2_PLACEMENT_3D ( 'NONE', #69554, #28657, #68657 ) ;
#27964=FACE_OUTER_BOUND ( 'NONE', #41622, .T. ) ;
#27970=LINE ( 'NONE', #55648, #43833 ) ;
#28033=VERTEX_POINT ( 'NONE', #86646 ) ;
#28045=VERTEX_POINT ( 'NONE', #4860 ) ;
#28082=DIRECTION ( 'NONE',  ( 0.000000000000000000, 1.000000000000000000, 0.000000000000000000 ) ) ;
#28133=ORIENTED_EDGE ( 'NONE', *, *, #33974, .T. ) ;
#28136=DIRECTION ( 'NONE',  ( 0.000000000000000000, 0.000000000000000000, -1.000000000000000000 ) ) ;
#28167=ORIENTED_EDGE ( 'NONE', *, *, #14107, .T. ) ;
#28173=CARTESIAN_POINT ( 'NONE',  ( 0.000000000000000000, 127.0000000000000000, 101.0189074266571794 ) ) ;
#28219=VECTOR ( 'NONE', #19269, 999.9999999999998863 ) ;
#28240=CARTESIAN_POINT ( 'NONE',  ( 0.000000000000000000, 211.0000000000000000, 164.6557476874258441 ) ) ;
#28324=ADVANCED_BREP_SHAPE_REPRESENTATION ( '', ( #80543, #50656 ), #23133 ) ;
#28383=EDGE_LOOP ( 'NONE', ( #66184, #65984, #75413, #5175 ) ) ;
#28404=ORIENTED_EDGE ( 'NONE', *, *, #41084, .F. ) ;
#28519=ORIENTED_EDGE ( 'NONE', *, *, #81384, .T. ) ;
#28544=ORIENTED_EDGE ( 'NONE', *, *, #26214, .T. ) ;
#28556=ORIENTED_EDGE ( 'NONE', *, *, #21492, .T. ) ;
#28557=EDGE_CURVE ( 'NONE', #78790, #38527, #46509, .T. ) ;
#28628=ORIENTED_EDGE ( 'NONE', *, *, #72825, .T. ) ;
#28630=CIRCLE ( 'NONE', #24291, 15.00000000000000000 ) ;
#28657=DIRECTION ( 'NONE',  ( 0.000000000000000000, 1.000000000000000000, 0.000000000000000000 ) ) ;
#28750=AXIS2_PLACEMENT_3D ( 'NONE', #78875, #71608, #24782 ) ;
#28777=PLANE ( 'NONE',  #70636 ) ;
#28894=VERTEX_POINT ( 'NONE', #67658 ) ;
#29130=DIRECTION ( 'NONE',  ( -0.6893610196960178182, -0.7071067811865296981, -0.1574210421884305322 ) ) ;
#29281=EDGE_CURVE ( 'NONE', #15679, #55444, #71695, .T. ) ;
#29301=CIRCLE ( 'NONE', #67018, 9.499999999999980460 ) ;
#29317=CARTESIAN_POINT ( 'NONE',  ( 0.000000000000000000, 239.0000000000000000, 154.6557476874258441 ) ) ;
#29332=FACE_OUTER_BOUND ( 'NONE', #54436, .T. ) ;
#29392=ADVANCED_FACE ( 'NONE', ( #24435 ), #87999, .F. ) ;
#29397=CARTESIAN_POINT ( 'NONE',  ( 27.27158787008325902, 127.0000000000000000, -5.920431057502157584E-15 ) ) ;
#29400=ORIENTED_EDGE ( 'NONE', *, *, #51140, .F. ) ;
#29530=CARTESIAN_POINT ( 'NONE',  ( 6.123233995736773185E-16, 215.0000000000000000, 149.6557476874258441 ) ) ;
#29549=VERTEX_POINT ( 'NONE', #13045 ) ;
#29586=VERTEX_POINT ( 'NONE', #48433 ) ;
#29619=PLANE ( 'NONE',  #738 ) ;
#29663=VECTOR ( 'NONE', #51092, 1000.000000000000000 ) ;
#29711=DIRECTION ( 'NONE',  ( 8.659560562355118980E-17, -0.7071067811865321406, 0.7071067811865628938 ) ) ;
#29715=ORIENTED_EDGE ( 'NONE', *, *, #3042, .T. ) ;
#29736=CIRCLE ( 'NONE', #71754, 7.199999999999998401 ) ;
#29763=ORIENTED_EDGE ( 'NONE', *, *, #39298, .F. ) ;
#29779=DIRECTION ( 'NONE',  ( 1.000000000000000000, -0.000000000000000000, 0.000000000000000000 ) ) ;
#29890=LINE ( 'NONE', #78044, #33664 ) ;
#29986=AXIS2_PLACEMENT_3D ( 'NONE', #7037, #216, #88379 ) ;
#30003=ORIENTED_EDGE ( 'NONE', *, *, #81384, .F. ) ;
#30036=CARTESIAN_POINT ( 'NONE',  ( 1.387778780781445676E-14, 238.8000000000000114, 97.27542076772557778 ) ) ;
#30069=LINE ( 'NONE', #64586, #46830 ) ;
#30343=PLANE ( 'NONE',  #72703 ) ;
#30355=DIRECTION ( 'NONE',  ( -2.170915417798913418E-16, 0.000000000000000000, -1.000000000000000000 ) ) ;
#30361=CARTESIAN_POINT ( 'NONE',  ( 1.387778780781445676E-14, 239.0000000000000000, 97.27542076772557778 ) ) ;
#30483=DIRECTION ( 'NONE',  ( 0.000000000000000000, 0.000000000000000000, 1.000000000000000000 ) ) ;
#30608=AXIS2_PLACEMENT_3D ( 'NONE', #79412, #87107, #23992 ) ;
#30624=PLANE ( 'NONE',  #15911 ) ;
#30687=AXIS2_PLACEMENT_3D ( 'NONE', #29317, #41568, #27508 ) ;
#30698=ORIENTED_EDGE ( 'NONE', *, *, #89616, .T. ) ;
#30788=TOROIDAL_SURFACE ( 'NONE', #43872, 9.000000000000007105, 1.000000000000000000 ) ;
#30823=ADVANCED_FACE ( 'NONE', ( #67573 ), #82125, .F. ) ;
#30873=PRESENTATION_STYLE_ASSIGNMENT (( #84966 ) ) ;
#30874=CARTESIAN_POINT ( 'NONE',  ( 27.27158787008325902, 184.0000000000000000, -5.920431057502157584E-15 ) ) ;
#30885=FACE_OUTER_BOUND ( 'NONE', #78430, .T. ) ;
#30994=FACE_OUTER_BOUND ( 'NONE', #86789, .T. ) ;
#31021=CARTESIAN_POINT ( 'NONE',  ( 0.000000000000000000, 239.0000000000000000, 154.6557476874258441 ) ) ;
#31109=DIRECTION ( 'NONE',  ( 0.000000000000000000, 1.000000000000000000, 0.000000000000000000 ) ) ;
#31125=ADVANCED_FACE ( 'NONE', ( #31154 ), #46558, .T. ) ;
#31154=FACE_OUTER_BOUND ( 'NONE', #63891, .T. ) ;
#31198=DIRECTION ( 'NONE',  ( 1.365069428641121829E-15, 0.000000000000000000, 1.000000000000000000 ) ) ;
#31203=DIRECTION ( 'NONE',  ( 2.170915417798913171E-16, 0.000000000000000000, 1.000000000000000000 ) ) ;
#31350=CIRCLE ( 'NONE', #82152, 7.199999999999998401 ) ;
#31354=ORIENTED_EDGE ( 'NONE', *, *, #78415, .F. ) ;
#31389=DIRECTION ( 'NONE',  ( -0.000000000000000000, -1.000000000000000000, -0.000000000000000000 ) ) ;
#31414=EDGE_LOOP ( 'NONE', ( #50059, #23645, #11840, #81256 ) ) ;
#31538=DIRECTION ( 'NONE',  ( 0.000000000000000000, -1.000000000000000000, 0.000000000000000000 ) ) ;
#31540=LINE ( 'NONE', #59243, #18674 ) ;
#31541=CARTESIAN_POINT ( 'NONE',  ( -13.40680633928205090, 223.9999999999999716, 102.7987842159323293 ) ) ;
#31661=AXIS2_PLACEMENT_3D ( 'NONE', #87628, #87014, #72493 ) ;
#31671=CYLINDRICAL_SURFACE ( 'NONE', #43162, 10.00000000000000888 ) ;
#31706=AXIS2_PLACEMENT_3D ( 'NONE', #7787, #22320, #71374 ) ;
#31716=EDGE_LOOP ( 'NONE', ( #35848, #7398, #71254, #65710, #53882, #53140, #67302, #73023, #20970, #24133, #49223, #72130, #25202, #63245, #52698, #36891, #60555, #28519, #35595, #86497 ) ) ;
#31779=AXIS2_PLACEMENT_3D ( 'NONE', #88838, #60195, #12076 ) ;
#31840=ORIENTED_EDGE ( 'NONE', *, *, #76869, .T. ) ;
#31870=ADVANCED_FACE ( 'NONE', ( #41425 ), #23055, .T. ) ;
#31918=EDGE_CURVE ( 'NONE', #42810, #78790, #38967, .T. ) ;
#31933=EDGE_CURVE ( 'NONE', #1202, #1599, #77315, .T. ) ;
#31937=CARTESIAN_POINT ( 'NONE',  ( 0.000000000000000000, 238.5000000000000000, 154.6557476874258441 ) ) ;
#31955=CIRCLE ( 'NONE', #85681, 1.000000000000000888 ) ;
#32017=AXIS2_PLACEMENT_3D ( 'NONE', #39053, #89917, #83534 ) ;
#32046=CARTESIAN_POINT ( 'NONE',  ( 0.000000000000000000, 239.0000000000000000, 154.6557476874258441 ) ) ;
#32083=DIRECTION ( 'NONE',  ( -0.000000000000000000, -1.000000000000000000, -0.000000000000000000 ) ) ;
#32152=CARTESIAN_POINT ( 'NONE',  ( -13.86911000615384104, 224.4999999999999432, 102.9892450244911828 ) ) ;
#32175=ORIENTED_EDGE ( 'NONE', *, *, #55931, .F. ) ;
#32194=CARTESIAN_POINT ( 'NONE',  ( -13.40680633928205090, 223.9999999999999716, 102.7987842159323293 ) ) ;
#32241=ORIENTED_EDGE ( 'NONE', *, *, #36045, .T. ) ;
#32244=FACE_OUTER_BOUND ( 'NONE', #84267, .T. ) ;
#32254=VECTOR ( 'NONE', #3024, 1000.000000000000000 ) ;
#32305=CIRCLE ( 'NONE', #33814, 7.199999999999998401 ) ;
#32337=EDGE_LOOP ( 'NONE', ( #29763, #32175, #67927, #35456 ) ) ;
#32399=DIRECTION ( 'NONE',  ( 1.000000000000000000, 0.000000000000000000, -2.544367396927093358E-16 ) ) ;
#32609=EDGE_CURVE ( 'NONE', #46763, #6826, #44802, .T. ) ;
#32628=ORIENTED_EDGE ( 'NONE', *, *, #25047, .F. ) ;
#32662=CARTESIAN_POINT ( 'NONE',  ( 0.000000000000000000, 127.0000000000000000, 90.32146847885337593 ) ) ;
#32696=FACE_OUTER_BOUND ( 'NONE', #41358, .T. ) ;
#32723=CARTESIAN_POINT ( 'NONE',  ( -89.60916260784479448, 224.4999999999999432, 134.1927865330827103 ) ) ;
#32825=LINE ( 'NONE', #81008, #8127 ) ;
#32907=APPLICATION_CONTEXT ( 'automotive_design' ) ;
#32966=EDGE_LOOP ( 'NONE', ( #56645, #73388, #49545, #13028 ) ) ;
#33062=ADVANCED_FACE ( 'NONE', ( #50612, #16115 ), #30624, .T. ) ;
#33144=LINE ( 'NONE', #20862, #53532 ) ;
#33227=CIRCLE ( 'NONE', #41888, 81.91591158490091118 ) ;
#33293=ORIENTED_EDGE ( 'NONE', *, *, #53022, .T. ) ;
#33416=ORIENTED_EDGE ( 'NONE', *, *, #20863, .T. ) ;
#33418=ORIENTED_EDGE ( 'NONE', *, *, #13588, .F. ) ;
#33428=DIRECTION ( 'NONE',  ( 0.000000000000000000, 0.000000000000000000, -1.000000000000000000 ) ) ;
#33432=VERTEX_POINT ( 'NONE', #20578 ) ;
#33455=ORIENTED_EDGE ( 'NONE', *, *, #14319, .T. ) ;
#33496=ORIENTED_EDGE ( 'NONE', *, *, #87626, .F. ) ;
#33506=ADVANCED_FACE ( 'NONE', ( #51379 ), #29619, .T. ) ;
#33574=ORIENTED_EDGE ( 'NONE', *, *, #16186, .T. ) ;
#33612=DIRECTION ( 'NONE',  ( -0.000000000000000000, -1.000000000000000000, -0.000000000000000000 ) ) ;
#33664=VECTOR ( 'NONE', #50304, 1000.000000000000000 ) ;
#33812=CARTESIAN_POINT ( 'NONE',  ( 0.000000000000000000, 184.0000000000000000, 85.23828826961327820 ) ) ;
#33814=AXIS2_PLACEMENT_3D ( 'NONE', #85238, #71598, #57501 ) ;
#33910=LINE ( 'NONE', #40272, #72676 ) ;
#33974=EDGE_CURVE ( 'NONE', #62958, #24524, #37058, .T. ) ;
#34015=ADVANCED_FACE ( 'NONE', ( #49943 ), #85845, .T. ) ;
#34090=VECTOR ( 'NONE', #7546, 1000.000000000000000 ) ;
#34129=ADVANCED_FACE ( 'NONE', ( #80765 ), #18518, .F. ) ;
#34280=CYLINDRICAL_SURFACE ( 'NONE', #29986, 10.00000000000000888 ) ;
#34281=CARTESIAN_POINT ( 'NONE',  ( 9.749037034254362410, 238.5000000000000000, 152.4294779587682740 ) ) ;
#34322=EDGE_LOOP ( 'NONE', ( #61501, #64681, #48578, #58871 ) ) ;
#34330=DIRECTION ( 'NONE',  ( 0.000000000000000000, 1.000000000000000000, 0.000000000000000000 ) ) ;
#34333=DIRECTION ( 'NONE',  ( 0.000000000000000000, 0.000000000000000000, -1.000000000000000000 ) ) ;
#34357=ORIENTED_EDGE ( 'NONE', *, *, #41906, .T. ) ;
#34375=CIRCLE ( 'NONE', #53208, 81.91591158490091118 ) ;
#34500=EDGE_LOOP ( 'NONE', ( #69244, #33496, #28628, #12947 ) ) ;
#34507=EDGE_CURVE ( 'NONE', #15778, #9020, #51468, .T. ) ;
#34600=EDGE_CURVE ( 'NONE', #73188, #28045, #60065, .T. ) ;
#34689=DIRECTION ( 'NONE',  ( -0.6893610196960194836, -0.7071067811865346942, 0.1574210421884011946 ) ) ;
#34830=LINE ( 'NONE', #313, #4302 ) ;
#34893=AXIS2_PLACEMENT_3D ( 'NONE', #59095, #3704, #10082 ) ;
#35030=LINE ( 'NONE', #75, #85780 ) ;
#35087=EDGE_CURVE ( 'NONE', #55007, #79794, #11383, .T. ) ;
#35104=AXIS2_PLACEMENT_3D ( 'NONE', #45659, #38420, #39319 ) ;
#35130=DIRECTION ( 'NONE',  ( 0.000000000000000000, 0.000000000000000000, 1.000000000000000000 ) ) ;
#35134=AXIS2_PLACEMENT_3D ( 'NONE', #13003, #66148, #73417 ) ;
#35149=LINE ( 'NONE', #65105, #38948 ) ;
#35162=CIRCLE ( 'NONE', #64172, 10.00000000000000888 ) ;
#35226=CARTESIAN_POINT ( 'NONE',  ( 27.27158787008325902, 184.0000000000000000, -5.920431057502157584E-15 ) ) ;
#35253=ORIENTED_EDGE ( 'NONE', *, *, #73704, .T. ) ;
#35456=ORIENTED_EDGE ( 'NONE', *, *, #12572, .T. ) ;
#35542=CARTESIAN_POINT ( 'NONE',  ( 6.123233995736768255E-16, 223.9999999999999716, 149.6557476874258441 ) ) ;
#35575=ORIENTED_EDGE ( 'NONE', *, *, #88582, .T. ) ;
#35595=ORIENTED_EDGE ( 'NONE', *, *, #72825, .F. ) ;
#35669=DIRECTION ( 'NONE',  ( 0.000000000000000000, 0.000000000000000000, 1.000000000000000000 ) ) ;
#35768=CARTESIAN_POINT ( 'NONE',  ( 0.000000000000000000, 215.0000000000000000, 159.6557476874258441 ) ) ;
#35790=CARTESIAN_POINT ( 'NONE',  ( 24.79284581386643183, 127.0000000000000000, 85.23828826961327820 ) ) ;
#35848=ORIENTED_EDGE ( 'NONE', *, *, #64640, .F. ) ;
#35956=ADVANCED_FACE ( 'NONE', ( #53811 ), #66330, .F. ) ;
#35980=FACE_OUTER_BOUND ( 'NONE', #12364, .T. ) ;
#36012=VECTOR ( 'NONE', #3192, 1000.000000000000000 ) ;
#36045=EDGE_CURVE ( 'NONE', #78613, #75146, #11230, .T. ) ;
#36257=ORIENTED_EDGE ( 'NONE', *, *, #41084, .T. ) ;
#36267=ORIENTED_EDGE ( 'NONE', *, *, #34507, .T. ) ;
#36279=FACE_OUTER_BOUND ( 'NONE', #77126, .T. ) ;
#36393=VECTOR ( 'NONE', #30355, 1000.000000000000000 ) ;
#36712=FACE_OUTER_BOUND ( 'NONE', #23989, .T. ) ;
#36891=ORIENTED_EDGE ( 'NONE', *, *, #72556, .F. ) ;
#36893=AXIS2_PLACEMENT_3D ( 'NONE', #46738, #10457, #66751 ) ;
#36898=CARTESIAN_POINT ( 'NONE',  ( 0.000000000000000000, 224.4999999999999432, 154.6557476874258441 ) ) ;
#36949=DIRECTION ( 'NONE',  ( 0.000000000000000000, -0.7071067811865291430, -0.7071067811865660024 ) ) ;
#36993=ORIENTED_EDGE ( 'NONE', *, *, #3006, .F. ) ;
#37020=EDGE_CURVE ( 'NONE', #11193, #42810, #89396, .T. ) ;
#37058=CIRCLE ( 'NONE', #77717, 10.00000000000000888 ) ;
#37160=DIRECTION ( 'NONE',  ( 0.000000000000000000, 0.000000000000000000, 1.000000000000000000 ) ) ;
#37162=EDGE_CURVE ( 'NONE', #64576, #46976, #11637, .T. ) ;
#37244=( LENGTH_UNIT ( ) NAMED_UNIT ( * ) SI_UNIT ( .MILLI., .METRE. ) );
#37304=AXIS2_PLACEMENT_3D ( 'NONE', #62889, #41098, #83352 ) ;
#37319=AXIS2_PLACEMENT_3D ( 'NONE', #61523, #55138, #76062 ) ;
#37331=DIRECTION ( 'NONE',  ( 0.000000000000000000, -0.000000000000000000, 1.000000000000000000 ) ) ;
#37341=CIRCLE ( 'NONE', #76505, 7.000000000000006217 ) ;
#37427=DIRECTION ( 'NONE',  ( -1.000000000000000000, 0.000000000000000000, 2.170915417798913171E-16 ) ) ;
#37478=LINE ( 'NONE', #31541, #26737 ) ;
#37497=DIRECTION ( 'NONE',  ( 0.000000000000000000, 0.000000000000000000, 1.000000000000000000 ) ) ;
#37517=EDGE_CURVE ( 'NONE', #43582, #22883, #60396, .T. ) ;
#37573=ORIENTED_EDGE ( 'NONE', *, *, #66295, .F. ) ;
#37615=EDGE_CURVE ( 'NONE', #73753, #75146, #55360, .T. ) ;
#37660=EDGE_CURVE ( 'NONE', #27566, #79794, #15854, .T. ) ;
#37684=ORIENTED_EDGE ( 'NONE', *, *, #83337, .F. ) ;
#37709=EDGE_CURVE ( 'NONE', #66435, #29549, #8597, .T. ) ;
#37783=DIRECTION ( 'NONE',  ( -1.000000000000000000, 0.000000000000000000, 0.000000000000000000 ) ) ;
#37847=DIRECTION ( 'NONE',  ( 0.000000000000000000, -1.000000000000000000, 0.000000000000000000 ) ) ;
#37962=CARTESIAN_POINT ( 'NONE',  ( 27.27158787008327678, 184.0000000000000000, 90.32146847885336172 ) ) ;
#38088=DIRECTION ( 'NONE',  ( 0.000000000000000000, 0.000000000000000000, 1.000000000000000000 ) ) ;
#38125=AXIS2_PLACEMENT_3D ( 'NONE', #88979, #61257, #88092 ) ;
#38238=ORIENTED_EDGE ( 'NONE', *, *, #86441, .F. ) ;
#38293=DIRECTION ( 'NONE',  ( 0.000000000000000000, -1.000000000000000000, 0.000000000000000000 ) ) ;
#38302=EDGE_CURVE ( 'NONE', #42810, #15084, #68405, .T. ) ;
#38351=CARTESIAN_POINT ( 'NONE',  ( 1.387778780781445676E-14, 239.0000000000000000, 97.27542076772557778 ) ) ;
#38352=ADVANCED_FACE ( 'NONE', ( #10093 ), #56195, .T. ) ;
#38371=DIRECTION ( 'NONE',  ( 0.000000000000000000, 1.000000000000000000, 0.000000000000000000 ) ) ;
#38420=DIRECTION ( 'NONE',  ( 0.000000000000000000, -1.000000000000000000, 0.000000000000000000 ) ) ;
#38510=EDGE_LOOP ( 'NONE', ( #39491, #82999, #2575, #65213, #56992, #20013, #11823, #65780, #20125, #86839, #9008, #5326, #66212, #33293, #69473, #89296, #57088, #18228, #26354, #20267 ) ) ;
#38527=VERTEX_POINT ( 'NONE', #88197 ) ;
#38552=CARTESIAN_POINT ( 'NONE',  ( -27.27158787008326968, 127.0000000000000000, -0.000000000000000000 ) ) ;
#38576=LINE ( 'NONE', #59461, #83091 ) ;
#38663=VERTEX_POINT ( 'NONE', #41351 ) ;
#38722=PRODUCT ( 'Pneumatic Toggle Clamp Unit', 'Pneumatic Toggle Clamp Unit', '', ( #39039 ) ) ;
#38778=FACE_OUTER_BOUND ( 'NONE', #9554, .T. ) ;
#38841=ORIENTED_EDGE ( 'NONE', *, *, #87626, .T. ) ;
#38876=DIRECTION ( 'NONE',  ( 0.000000000000000000, 0.000000000000000000, 1.000000000000000000 ) ) ;
#38933=ORIENTED_EDGE ( 'NONE', *, *, #64640, .T. ) ;
#38948=VECTOR ( 'NONE', #51021, 1000.000000000000000 ) ;
#38967=CIRCLE ( 'NONE', #86836, 5.000000000000004441 ) ;
#39039=PRODUCT_CONTEXT ( 'NONE', #71799, 'mechanical' ) ;
#39053=CARTESIAN_POINT ( 'NONE',  ( 24.79284581386629327, 184.0000000000000000, -3.384395586952189366E-14 ) ) ;
#39061=DIRECTION ( 'NONE',  ( -1.000000000000000000, 0.000000000000000000, -0.000000000000000000 ) ) ;
#39103=EDGE_CURVE ( 'NONE', #78613, #41873, #13555, .T. ) ;
#39255=CARTESIAN_POINT ( 'NONE',  ( 0.000000000000000000, 223.9999999999999716, 0.000000000000000000 ) ) ;
#39298=EDGE_CURVE ( 'NONE', #48100, #55376, #59349, .T. ) ;
#39319=DIRECTION ( 'NONE',  ( 0.000000000000000000, 0.000000000000000000, -1.000000000000000000 ) ) ;
#39431=ADVANCED_FACE ( 'NONE', ( #73432 ), #4406, .F. ) ;
#39485=CARTESIAN_POINT ( 'NONE',  ( -27.27158787008326968, 127.0000000000000000, 85.23828826961327820 ) ) ;
#39491=ORIENTED_EDGE ( 'NONE', *, *, #62919, .T. ) ;
#39516=DIRECTION ( 'NONE',  ( -1.000000000000000000, 0.000000000000000000, 0.000000000000000000 ) ) ;
#39544=CARTESIAN_POINT ( 'NONE',  ( 0.000000000000000000, 184.0000000000000000, 106.1020876358972629 ) ) ;
#39635=DIRECTION ( 'NONE',  ( 0.000000000000000000, 0.000000000000000000, -1.000000000000000000 ) ) ;
#39718=CARTESIAN_POINT ( 'NONE',  ( 2.036081061455522238E-14, 184.0000000000000000, 80.02307622376218887 ) ) ;
#39747=ORIENTED_EDGE ( 'NONE', *, *, #89616, .F. ) ;
#39754=VECTOR ( 'NONE', #82172, 1000.000000000000000 ) ;
#39866=ORIENTED_EDGE ( 'NONE', *, *, #50617, .F. ) ;
#39928=EDGE_LOOP ( 'NONE', ( #77539, #82588, #39747, #352 ) ) ;
#39953=CARTESIAN_POINT ( 'NONE',  ( 0.000000000000000000, 127.0000000000000000, 106.1020876358972629 ) ) ;
#39960=CARTESIAN_POINT ( 'NONE',  ( 1.387778780781445676E-14, 239.0000000000000000, 90.27542076772557778 ) ) ;
#40272=CARTESIAN_POINT ( 'NONE',  ( 24.79284581386643183, 184.0000000000000000, 85.23828826961327820 ) ) ;
#40350=VECTOR ( 'NONE', #59908, 1000.000000000000000 ) ;
#40352=ORIENTED_EDGE ( 'NONE', *, *, #46643, .F. ) ;
#40397=EDGE_CURVE ( 'NONE', #4973, #78353, #20839, .T. ) ;
#40424=CARTESIAN_POINT ( 'NONE',  ( -24.79284581386642827, 184.0000000000000000, 85.23828826961327820 ) ) ;
#40468=ORIENTED_EDGE ( 'NONE', *, *, #42312, .T. ) ;
#40537=FACE_OUTER_BOUND ( 'NONE', #70594, .T. ) ;
#40603=PLANE ( 'NONE',  #69196 ) ;
#40641=CARTESIAN_POINT ( 'NONE',  ( 9.261585182541649530, 223.9999999999999716, 152.5407914452011369 ) ) ;
#40664=ORIENTED_EDGE ( 'NONE', *, *, #88146, .F. ) ;
#40732=DIRECTION ( 'NONE',  ( -0.000000000000000000, -1.000000000000000000, 0.000000000000000000 ) ) ;
#40744=ADVANCED_FACE ( 'NONE', ( #53425 ), #31671, .T. ) ;
#40880=ADVANCED_FACE ( 'NONE', ( #9789 ), #2539, .F. ) ;
#40882=PLANE ( 'NONE',  #71806 ) ;
#40972=CARTESIAN_POINT ( 'NONE',  ( 24.79284581386643183, 127.0000000000000000, 90.32146847885336172 ) ) ;
#40979=CARTESIAN_POINT ( 'NONE',  ( 24.79284581386629327, 184.0000000000000000, -3.384395586952189366E-14 ) ) ;
#41026=TOROIDAL_SURFACE ( 'NONE', #51211, 9.000000000000007105, 1.000000000000000000 ) ;
#41084=EDGE_CURVE ( 'NONE', #43582, #17076, #37341, .T. ) ;
#41098=DIRECTION ( 'NONE',  ( -0.000000000000000000, -1.000000000000000000, 0.000000000000000000 ) ) ;
#41146=FACE_OUTER_BOUND ( 'NONE', #53577, .T. ) ;
#41350=DIRECTION ( 'NONE',  ( 0.000000000000000000, 0.000000000000000000, 1.000000000000000000 ) ) ;
#41351=CARTESIAN_POINT ( 'NONE',  ( 13.40680633928208465, 223.9999999999999716, 102.7987842159323151 ) ) ;
#41358=EDGE_LOOP ( 'NONE', ( #87389, #50491, #33574, #28556 ) ) ;
#41375=FACE_OUTER_BOUND ( 'NONE', #85617, .T. ) ;
#41398=DIRECTION ( 'NONE',  ( 0.000000000000000000, -1.000000000000000000, 0.000000000000000000 ) ) ;
#41425=FACE_OUTER_BOUND ( 'NONE', #10074, .T. ) ;
#41461=EDGE_CURVE ( 'NONE', #17964, #27454, #88190, .T. ) ;
#41568=DIRECTION ( 'NONE',  ( 0.000000000000000000, 1.000000000000000000, 0.000000000000000000 ) ) ;
#41622=EDGE_LOOP ( 'NONE', ( #9968, #47731, #79480, #84575 ) ) ;
#41712=AXIS2_PLACEMENT_3D ( 'NONE', #55011, #41398, #13714 ) ;
#41790=ORIENTED_EDGE ( 'NONE', *, *, #67620, .F. ) ;
#41873=VERTEX_POINT ( 'NONE', #72647 ) ;
#41888=AXIS2_PLACEMENT_3D ( 'NONE', #6209, #68876, #89331 ) ;
#41906=EDGE_CURVE ( 'NONE', #23939, #14672, #51565, .T. ) ;
#41938=CARTESIAN_POINT ( 'NONE',  ( 1.387778780781445676E-14, 223.9999999999999716, 97.27542076772557778 ) ) ;
#42038=DIRECTION ( 'NONE',  ( 2.170915417798913171E-16, 0.000000000000000000, 1.000000000000000000 ) ) ;
#42120=AXIS2_PLACEMENT_3D ( 'NONE', #80116, #37427, #66004 ) ;
#42204=VECTOR ( 'NONE', #42913, 1000.000000000000000 ) ;
#42251=FACE_OUTER_BOUND ( 'NONE', #198, .T. ) ;
#42312=EDGE_CURVE ( 'NONE', #51214, #73315, #35149, .T. ) ;
#42371=CARTESIAN_POINT ( 'NONE',  ( 0.000000000000000000, 224.4999999999999432, 154.6557476874258441 ) ) ;
#42571=DIRECTION ( 'NONE',  ( 0.000000000000000000, 0.000000000000000000, 1.000000000000000000 ) ) ;
#42594=VERTEX_POINT ( 'NONE', #68685 ) ;
#42686=( NAMED_UNIT ( * ) SI_UNIT ( $, .STERADIAN. ) SOLID_ANGLE_UNIT ( ) );
#42743=VERTEX_POINT ( 'NONE', #10371 ) ;
#42763=DIRECTION ( 'NONE',  ( -0.000000000000000000, -1.000000000000000000, -0.000000000000000000 ) ) ;
#42810=VERTEX_POINT ( 'NONE', #47997 ) ;
#42823=EDGE_CURVE ( 'NONE', #33432, #79965, #81056, .T. ) ;
#42840=ORIENTED_EDGE ( 'NONE', *, *, #29281, .F. ) ;
#42913=DIRECTION ( 'NONE',  ( -0.000000000000000000, 1.000000000000000000, -0.000000000000000000 ) ) ;
#43144=FILL_AREA_STYLE_COLOUR ( '', #74751 ) ;
#43162=AXIS2_PLACEMENT_3D ( 'NONE', #17166, #5318, #18039 ) ;
#43230=ADVANCED_FACE ( 'NONE', ( #7477 ), #23108, .F. ) ;
#43231=CARTESIAN_POINT ( 'NONE',  ( 2.036081061455522238E-14, 184.0000000000000000, 80.02307622376218887 ) ) ;
#43238=CARTESIAN_POINT ( 'NONE',  ( 27.27158787008327678, 127.0000000000000000, 101.0189074266571794 ) ) ;
#43276=CARTESIAN_POINT ( 'NONE',  ( -27.27158787008326968, 184.0000000000000000, 0.000000000000000000 ) ) ;
#43356=EDGE_LOOP ( 'NONE', ( #1005, #49904 ) ) ;
#43444=LINE ( 'NONE', #29397, #32254 ) ;
#43582=VERTEX_POINT ( 'NONE', #3789 ) ;
#43738=CARTESIAN_POINT ( 'NONE',  ( 0.000000000000000000, 211.0000000000000000, 145.6557476874258441 ) ) ;
#43793=CARTESIAN_POINT ( 'NONE',  ( 0.000000000000000000, 184.0000000000000000, 0.000000000000000000 ) ) ;
#43833=VECTOR ( 'NONE', #29779, 1000.000000000000000 ) ;
#43862=VERTEX_POINT ( 'NONE', #28240 ) ;
#43872=AXIS2_PLACEMENT_3D ( 'NONE', #84600, #54261, #47008 ) ;
#43946=CARTESIAN_POINT ( 'NONE',  ( -27.27158787008326968, 184.0000000000000000, 0.000000000000000000 ) ) ;
#44034=( NAMED_UNIT ( * ) PLANE_ANGLE_UNIT ( ) SI_UNIT ( $, .RADIAN. ) );
#44077=CIRCLE ( 'NONE', #80413, 5.000000000000004441 ) ;
#44126=LINE ( 'NONE', #15104, #1456 ) ;
#44164=DIRECTION ( 'NONE',  ( 0.000000000000000000, -0.000000000000000000, 1.000000000000000000 ) ) ;
#44244=EDGE_CURVE ( 'NONE', #67055, #48933, #55374, .T. ) ;
#44296=ORIENTED_EDGE ( 'NONE', *, *, #25920, .F. ) ;
#44300=DIRECTION ( 'NONE',  ( 0.000000000000000000, 1.000000000000000000, -0.000000000000000000 ) ) ;
#44565=LINE ( 'NONE', #1917, #7696 ) ;
#44600=ORIENTED_EDGE ( 'NONE', *, *, #12060, .F. ) ;
#44605=SURFACE_STYLE_USAGE ( .BOTH. , #59128 ) ;
#44664=EDGE_CURVE ( 'NONE', #78126, #14672, #85720, .T. ) ;
#44722=PLANE ( 'NONE',  #75747 ) ;
#44735=CARTESIAN_POINT ( 'NONE',  ( 1.387778780781445676E-14, 239.0000000000000000, 97.27542076772557778 ) ) ;
#44762=VERTEX_POINT ( 'NONE', #53924 ) ;
#44802=CIRCLE ( 'NONE', #31779, 14.49999999999997158 ) ;
#44804=ORIENTED_EDGE ( 'NONE', *, *, #20585, .F. ) ;
#45004=CARTESIAN_POINT ( 'NONE',  ( -27.27158787008326968, 127.0000000000000000, -0.000000000000000000 ) ) ;
#45025=AXIS2_PLACEMENT_3D ( 'NONE', #67130, #4466, #38088 ) ;
#45346=VERTEX_POINT ( 'NONE', #65068 ) ;
#45364=CIRCLE ( 'NONE', #38125, 5.000000000000004441 ) ;
#45373=CIRCLE ( 'NONE', #49728, 10.00000000000000888 ) ;
#45381=CARTESIAN_POINT ( 'NONE',  ( 1.475953350320055108E-14, 239.0000000000000000, 90.07542076772557493 ) ) ;
#45382=DIRECTION ( 'NONE',  ( 1.776356839400250465E-15, 0.000000000000000000, 1.000000000000000000 ) ) ;
#45489=LINE ( 'NONE', #71900, #83991 ) ;
#45490=DIRECTION ( 'NONE',  ( 1.000000000000000000, 0.000000000000000000, 0.000000000000000000 ) ) ;
#45492=CARTESIAN_POINT ( 'NONE',  ( 0.000000000000000000, 184.0000000000000000, 101.0189074266571794 ) ) ;
#45563=ORIENTED_EDGE ( 'NONE', *, *, #32609, .T. ) ;
#45630=ORIENTED_EDGE ( 'NONE', *, *, #55961, .F. ) ;
#45643=AXIS2_PLACEMENT_3D ( 'NONE', #48208, #70479, #55465 ) ;
#45659=CARTESIAN_POINT ( 'NONE',  ( 89.60916260784479448, 224.4999999999999432, 134.1927865330827103 ) ) ;
#45670=EDGE_LOOP ( 'NONE', ( #57657, #27653, #5158, #88902 ) ) ;
#45706=PLANE ( 'NONE',  #1706 ) ;
#45733=DIRECTION ( 'NONE',  ( 0.000000000000000000, 0.000000000000000000, -1.000000000000000000 ) ) ;
#45742=CONICAL_SURFACE ( 'NONE', #66050, 4.799999999999970512, 0.7853981633975198884 ) ;
#45848=AXIS2_PLACEMENT_3D ( 'NONE', #39718, #60152, #87889 ) ;
#45924=ORIENTED_EDGE ( 'NONE', *, *, #31918, .T. ) ;
#46044=PLANE ( 'NONE',  #52883 ) ;
#46069=DIRECTION ( 'NONE',  ( 1.000000000000000000, -0.000000000000000000, 0.000000000000000000 ) ) ;
#46109=DIRECTION ( 'NONE',  ( -0.000000000000000000, -1.000000000000000000, -0.000000000000000000 ) ) ;
#46124=EDGE_LOOP ( 'NONE', ( #12896, #1043, #28133, #18331 ) ) ;
#46257=DIRECTION ( 'NONE',  ( 0.000000000000000000, 0.000000000000000000, -1.000000000000000000 ) ) ;
#46314=EDGE_CURVE ( 'NONE', #82100, #78126, #29301, .T. ) ;
#46445=LINE ( 'NONE', #5133, #5509 ) ;
#46509=LINE ( 'NONE', #67869, #22007 ) ;
#46558=PLANE ( 'NONE',  #67032 ) ;
#46575=EDGE_LOOP ( 'NONE', ( #15922, #45924, #52769, #60634 ) ) ;
#46643=EDGE_CURVE ( 'NONE', #54446, #87703, #33910, .T. ) ;
#46730=ORIENTED_EDGE ( 'NONE', *, *, #54099, .F. ) ;
#46738=CARTESIAN_POINT ( 'NONE',  ( 0.000000000000000000, 239.0000000000000000, 154.6557476874258441 ) ) ;
#46763=VERTEX_POINT ( 'NONE', #57033 ) ;
#46810=ORIENTED_EDGE ( 'NONE', *, *, #55977, .F. ) ;
#46830=VECTOR ( 'NONE', #85501, 1000.000000000000000 ) ;
#46884=ORIENTED_EDGE ( 'NONE', *, *, #77664, .T. ) ;
#46930=ORIENTED_EDGE ( 'NONE', *, *, #80565, .T. ) ;
#46967=EDGE_LOOP ( 'NONE', ( #85173, #73512, #40468, #38841 ) ) ;
#46976=VERTEX_POINT ( 'NONE', #65204 ) ;
#46982=VECTOR ( 'NONE', #84177, 1000.000000000000000 ) ;
#46998=DIRECTION ( 'NONE',  ( 0.000000000000000000, 1.000000000000000000, 0.000000000000000000 ) ) ;
#47008=DIRECTION ( 'NONE',  ( 0.000000000000000000, 0.000000000000000000, -1.000000000000000000 ) ) ;
#47069=DIRECTION ( 'NONE',  ( -0.000000000000000000, -1.000000000000000000, -0.000000000000000000 ) ) ;
#47077=ORIENTED_EDGE ( 'NONE', *, *, #3042, .F. ) ;
#47261=VECTOR ( 'NONE', #29711, 1000.000000000000000 ) ;
#47318=DIRECTION ( 'NONE',  ( 0.000000000000000000, 1.000000000000000000, 0.000000000000000000 ) ) ;
#47422=CARTESIAN_POINT ( 'NONE',  ( 0.000000000000000000, 184.0000000000000000, 90.32146847885336172 ) ) ;
#47636=EDGE_LOOP ( 'NONE', ( #64378, #71766, #70622, #29400 ) ) ;
#47724=VECTOR ( 'NONE', #84155, 1000.000000000000000 ) ;
#47731=ORIENTED_EDGE ( 'NONE', *, *, #22014, .T. ) ;
#47749=ORIENTED_EDGE ( 'NONE', *, *, #83046, .F. ) ;
#47867=VECTOR ( 'NONE', #20610, 1000.000000000000000 ) ;
#47945=DIRECTION ( 'NONE',  ( -0.000000000000000000, -1.000000000000000000, -0.000000000000000000 ) ) ;
#47997=CARTESIAN_POINT ( 'NONE',  ( 6.123233995736769241E-16, 238.7999999999999829, 149.6557476874258441 ) ) ;
#48010=ORIENTED_EDGE ( 'NONE', *, *, #57080, .F. ) ;
#48070=ORIENTED_EDGE ( 'NONE', *, *, #36045, .F. ) ;
#48100=VERTEX_POINT ( 'NONE', #6677 ) ;
#48208=CARTESIAN_POINT ( 'NONE',  ( 24.79284581386643183, 184.0000000000000000, 0.000000000000000000 ) ) ;
#48232=EDGE_CURVE ( 'NONE', #75146, #80780, #52877, .T. ) ;
#48236=DIRECTION ( 'NONE',  ( -0.000000000000000000, -1.000000000000000000, -0.000000000000000000 ) ) ;
#48237=DIRECTION ( 'NONE',  ( 0.000000000000000000, 0.000000000000000000, 1.000000000000000000 ) ) ;
#48278=CARTESIAN_POINT ( 'NONE',  ( 27.27158787008327678, 127.0000000000000000, 90.32146847885336172 ) ) ;
#48342=VECTOR ( 'NONE', #60912, 1000.000000000000000 ) ;
#48358=ORIENTED_EDGE ( 'NONE', *, *, #7648, .T. ) ;
#48433=CARTESIAN_POINT ( 'NONE',  ( 1.224646799147354440E-15, 211.0000000000000000, 144.6557476874258441 ) ) ;
#48578=ORIENTED_EDGE ( 'NONE', *, *, #2093, .T. ) ;
#48691=VERTEX_POINT ( 'NONE', #643 ) ;
#48726=LINE ( 'NONE', #13348, #55116 ) ;
#48780=VECTOR ( 'NONE', #54440, 999.9999999999998863 ) ;
#48826=LINE ( 'NONE', #1617, #42204 ) ;
#48882=VECTOR ( 'NONE', #337, 1000.000000000000000 ) ;
#48933=VERTEX_POINT ( 'NONE', #40972 ) ;
#48955=CARTESIAN_POINT ( 'NONE',  ( -27.27158787008326968, 184.0000000000000000, 106.1020876358972771 ) ) ;
#49202=DIRECTION ( 'NONE',  ( 0.000000000000000000, 0.000000000000000000, 1.000000000000000000 ) ) ;
#49223=ORIENTED_EDGE ( 'NONE', *, *, #71114, .F. ) ;
#49306=DIRECTION ( 'NONE',  ( 0.000000000000000000, 0.000000000000000000, 1.000000000000000000 ) ) ;
#49356=VECTOR ( 'NONE', #66736, 1000.000000000000000 ) ;
#49390=DIRECTION ( 'NONE',  ( 0.000000000000000000, 1.000000000000000000, 0.000000000000000000 ) ) ;
#49452=ORIENTED_EDGE ( 'NONE', *, *, #10407, .F. ) ;
#49498=CARTESIAN_POINT ( 'NONE',  ( 0.000000000000000000, 184.0000000000000000, 106.1020876358972771 ) ) ;
#49545=ORIENTED_EDGE ( 'NONE', *, *, #41906, .F. ) ;
#49641=CARTESIAN_POINT ( 'NONE',  ( 0.000000000000000000, 239.0000000000000000, 154.6557476874258441 ) ) ;
#49727=EDGE_LOOP ( 'NONE', ( #86176, #21817, #61101, #12856 ) ) ;
#49728=AXIS2_PLACEMENT_3D ( 'NONE', #42371, #70100, #27861 ) ;
#49751=CARTESIAN_POINT ( 'NONE',  ( -9.261585182541640648, 223.9999999999999716, 152.5407914452011084 ) ) ;
#49752=DIRECTION ( 'NONE',  ( -0.000000000000000000, 1.000000000000000000, -0.000000000000000000 ) ) ;
#49834=CARTESIAN_POINT ( 'NONE',  ( -27.27158787008326968, 184.0000000000000000, 106.1020876358972771 ) ) ;
#49864=DIRECTION ( 'NONE',  ( -1.000000000000000000, 0.000000000000000000, 0.000000000000000000 ) ) ;
#49879=ADVANCED_FACE ( 'NONE', ( #6585 ), #34280, .T. ) ;
#49904=ORIENTED_EDGE ( 'NONE', *, *, #9816, .T. ) ;
#49943=FACE_OUTER_BOUND ( 'NONE', #45670, .T. ) ;
#50059=ORIENTED_EDGE ( 'NONE', *, *, #1906, .T. ) ;
#50153=ORIENTED_EDGE ( 'NONE', *, *, #14524, .F. ) ;
#50245=CARTESIAN_POINT ( 'NONE',  ( -24.79284581386642827, 127.0000000000000000, 101.0189074266571794 ) ) ;
#50304=DIRECTION ( 'NONE',  ( -2.170915417798913418E-16, 0.000000000000000000, -1.000000000000000000 ) ) ;
#50461=DIRECTION ( 'NONE',  ( 0.000000000000000000, -1.000000000000000000, 0.000000000000000000 ) ) ;
#50491=ORIENTED_EDGE ( 'NONE', *, *, #88582, .F. ) ;
#50532=ORIENTED_EDGE ( 'NONE', *, *, #14310, .T. ) ;
#50556=CARTESIAN_POINT ( 'NONE',  ( 9.749037034254360634, 224.4999999999999432, 152.4294779587682740 ) ) ;
#50612=FACE_BOUND ( 'NONE', #26388, .T. ) ;
#50617=EDGE_CURVE ( 'NONE', #11707, #73753, #34375, .T. ) ;
#50656=AXIS2_PLACEMENT_3D ( 'NONE', #89656, #19265, #5642 ) ;
#50678=VECTOR ( 'NONE', #1389, 1000.000000000000000 ) ;
#50692=DIRECTION ( 'NONE',  ( 0.000000000000000000, 1.000000000000000000, -0.000000000000000000 ) ) ;
#50732=ADVANCED_FACE ( 'NONE', ( #62218 ), #61991, .T. ) ;
#50964=ORIENTED_EDGE ( 'NONE', *, *, #61362, .F. ) ;
#50984=PRESENTATION_STYLE_ASSIGNMENT (( #44605 ) ) ;
#51021=DIRECTION ( 'NONE',  ( 0.000000000000000000, 0.000000000000000000, -1.000000000000000000 ) ) ;
#51092=DIRECTION ( 'NONE',  ( -0.000000000000000000, -1.000000000000000000, -0.000000000000000000 ) ) ;
#51140=EDGE_CURVE ( 'NONE', #76315, #59415, #62562, .T. ) ;
#51211=AXIS2_PLACEMENT_3D ( 'NONE', #63720, #52183, #17701 ) ;
#51214=VERTEX_POINT ( 'NONE', #12035 ) ;
#51379=FACE_OUTER_BOUND ( 'NONE', #12881, .T. ) ;
#51417=SURFACE_STYLE_FILL_AREA ( #85088 ) ;
#51468=LINE ( 'NONE', #11041, #63243 ) ;
#51544=CARTESIAN_POINT ( 'NONE',  ( 0.000000000000000000, 215.0000000000000000, 154.6557476874258441 ) ) ;
#51565=LINE ( 'NONE', #15739, #65026 ) ;
#51590=( GEOMETRIC_REPRESENTATION_CONTEXT ( 3 ) GLOBAL_UNCERTAINTY_ASSIGNED_CONTEXT ( ( #16926 ) ) GLOBAL_UNIT_ASSIGNED_CONTEXT ( ( #37244, #44034, #42686 ) ) REPRESENTATION_CONTEXT ( 'NONE', 'WORKASPACE' ) );
#51593=LINE ( 'NONE', #66914, #4945 ) ;
#51671=CARTESIAN_POINT ( 'NONE',  ( 27.27158787008327678, 184.0000000000000000, 85.23828826961327820 ) ) ;
#51859=( LENGTH_UNIT ( ) NAMED_UNIT ( * ) SI_UNIT ( .MILLI., .METRE. ) );
#51910=ORIENTED_EDGE ( 'NONE', *, *, #27765, .F. ) ;
#51952=ORIENTED_EDGE ( 'NONE', *, *, #55152, .T. ) ;
#51988=VECTOR ( 'NONE', #42763, 1000.000000000000000 ) ;
#52023=CARTESIAN_POINT ( 'NONE',  ( -24.79284581386642827, 127.0000000000000000, 0.000000000000000000 ) ) ;
#52102=FACE_OUTER_BOUND ( 'NONE', #20841, .T. ) ;
#52183=DIRECTION ( 'NONE',  ( 0.000000000000000000, -1.000000000000000000, 0.000000000000000000 ) ) ;
#52223=DIRECTION ( 'NONE',  ( 0.000000000000000000, 1.000000000000000000, -0.000000000000000000 ) ) ;
#52229=ORIENTED_EDGE ( 'NONE', *, *, #20863, .F. ) ;
#52432=CARTESIAN_POINT ( 'NONE',  ( 1.387778780781445676E-14, 239.0000000000000000, 97.27542076772557778 ) ) ;
#52472=ORIENTED_EDGE ( 'NONE', *, *, #84726, .F. ) ;
#52480=CARTESIAN_POINT ( 'NONE',  ( 27.27158787008328389, 184.0000000000000000, 111.9860621927989683 ) ) ;
#52536=CONICAL_SURFACE ( 'NONE', #35104, 81.91591158490091118, 0.7853981633974760346 ) ;
#52698=ORIENTED_EDGE ( 'NONE', *, *, #16186, .F. ) ;
#52726=EDGE_CURVE ( 'NONE', #9140, #42594, #63426, .T. ) ;
#52769=ORIENTED_EDGE ( 'NONE', *, *, #28557, .T. ) ;
#52781=DIRECTION ( 'NONE',  ( -1.000000000000000000, 0.000000000000000000, 0.000000000000000000 ) ) ;
#52877=CIRCLE ( 'NONE', #58743, 82.41591158490091118 ) ;
#52883=AXIS2_PLACEMENT_3D ( 'NONE', #39255, #66963, #4743 ) ;
#52887=CARTESIAN_POINT ( 'NONE',  ( 0.000000000000000000, 223.9999999999999716, 164.6557476874258441 ) ) ;
#52956=EDGE_CURVE ( 'NONE', #15070, #12137, #66525, .T. ) ;
#52971=AXIS2_PLACEMENT_3D ( 'NONE', #11359, #88576, #39061 ) ;
#52988=AXIS2_PLACEMENT_3D ( 'NONE', #2731, #24067, #65393 ) ;
#53004=AXIS2_PLACEMENT_3D ( 'NONE', #19519, #39516, #12718 ) ;
#53022=EDGE_CURVE ( 'NONE', #87703, #48933, #56355, .T. ) ;
#53024=CARTESIAN_POINT ( 'NONE',  ( 1.474728703520907694E-14, 239.0000000000000000, 104.2754207677255920 ) ) ;
#53040=DIRECTION ( 'NONE',  ( 0.000000000000000000, 0.000000000000000000, -1.000000000000000000 ) ) ;
#53058=DIRECTION ( 'NONE',  ( 0.000000000000000000, -1.000000000000000000, 0.000000000000000000 ) ) ;
#53100=VECTOR ( 'NONE', #46069, 1000.000000000000000 ) ;
#53103=PLANE ( 'NONE',  #52971 ) ;
#53140=ORIENTED_EDGE ( 'NONE', *, *, #29281, .T. ) ;
#53174=CARTESIAN_POINT ( 'NONE',  ( 0.000000000000000000, 239.0000000000000000, 154.6557476874258441 ) ) ;
#53201=AXIS2_PLACEMENT_3D ( 'NONE', #51544, #31109, #70679 ) ;
#53208=AXIS2_PLACEMENT_3D ( 'NONE', #32723, #82245, #88161 ) ;
#53266=VECTOR ( 'NONE', #88407, 1000.000000000000000 ) ;
#53277=PLANE ( 'NONE',  #19506 ) ;
#53323=ORIENTED_EDGE ( 'NONE', *, *, #53022, .F. ) ;
#53390=CARTESIAN_POINT ( 'NONE',  ( 0.000000000000000000, 184.0000000000000000, 106.1020876358972771 ) ) ;
#53393=ORIENTED_EDGE ( 'NONE', *, *, #37162, .F. ) ;
#53425=FACE_OUTER_BOUND ( 'NONE', #17231, .T. ) ;
#53441=CARTESIAN_POINT ( 'NONE',  ( 0.000000000000000000, 215.0000000000000000, 154.6557476874258441 ) ) ;
#53528=UNCERTAINTY_MEASURE_WITH_UNIT (LENGTH_MEASURE( 1.000000000000000082E-05 ), #22403, 'distance_accuracy_value', 'NONE');
#53532=VECTOR ( 'NONE', #53556, 1000.000000000000000 ) ;
#53542=VECTOR ( 'NONE', #70974, 1000.000000000000000 ) ;
#53556=DIRECTION ( 'NONE',  ( -1.000000000000000000, 0.000000000000000000, 2.544367396927093851E-16 ) ) ;
#53577=EDGE_LOOP ( 'NONE', ( #74045, #76352, #47749, #67775 ) ) ;
#53596=FACE_OUTER_BOUND ( 'NONE', #77336, .T. ) ;
#53616=ORIENTED_EDGE ( 'NONE', *, *, #83235, .F. ) ;
#53811=FACE_OUTER_BOUND ( 'NONE', #22119, .T. ) ;
#53823=DIRECTION ( 'NONE',  ( -0.000000000000000000, -1.000000000000000000, 0.000000000000000000 ) ) ;
#53882=ORIENTED_EDGE ( 'NONE', *, *, #71780, .F. ) ;
#53887=EDGE_LOOP ( 'NONE', ( #74698, #24623, #50153, #66971 ) ) ;
#53924=CARTESIAN_POINT ( 'NONE',  ( 1.387778780781445676E-14, 238.5000000000000000, 82.27542076772557778 ) ) ;
#53933=CARTESIAN_POINT ( 'NONE',  ( 6.000769315822015949E-16, 239.0000000000000000, 159.4557476874258271 ) ) ;
#54078=ORIENTED_EDGE ( 'NONE', *, *, #89595, .F. ) ;
#54098=DIRECTION ( 'NONE',  ( 0.000000000000000000, 1.000000000000000000, 0.000000000000000000 ) ) ;
#54099=EDGE_CURVE ( 'NONE', #76315, #22883, #32305, .T. ) ;
#54261=DIRECTION ( 'NONE',  ( 0.000000000000000000, -1.000000000000000000, 0.000000000000000000 ) ) ;
#54436=EDGE_LOOP ( 'NONE', ( #28544, #77540, #42840, #83794 ) ) ;
#54440=DIRECTION ( 'NONE',  ( 0.6537961156249192385, 0.7071067811865345831, 0.2693522585644786416 ) ) ;
#54446=VERTEX_POINT ( 'NONE', #14278 ) ;
#54493=CIRCLE ( 'NONE', #58853, 7.199999999999998401 ) ;
#54564=ADVANCED_FACE ( 'NONE', ( #86012 ), #59853, .T. ) ;
#54761=CARTESIAN_POINT ( 'NONE',  ( 0.000000000000000000, 223.9999999999999716, 154.6557476874258441 ) ) ;
#54811=EDGE_LOOP ( 'NONE', ( #22941, #64335, #24029, #30698, #67787 ) ) ;
#54877=DIRECTION ( 'NONE',  ( -0.000000000000000000, -1.000000000000000000, -0.000000000000000000 ) ) ;
#54944=EDGE_LOOP ( 'NONE', ( #79270, #67000, #84352, #17628 ) ) ;
#54965=DIRECTION ( 'NONE',  ( 0.000000000000000000, 1.000000000000000000, -0.000000000000000000 ) ) ;
#54971=AXIS2_PLACEMENT_3D ( 'NONE', #61924, #68754, #12447 ) ;
#55007=VERTEX_POINT ( 'NONE', #84112 ) ;
#55011=CARTESIAN_POINT ( 'NONE',  ( 1.387778780781445676E-14, 238.5000000000000000, 97.27542076772557778 ) ) ;
#55116=VECTOR ( 'NONE', #81955, 1000.000000000000000 ) ;
#55138=DIRECTION ( 'NONE',  ( 0.000000000000000000, 1.000000000000000000, -0.000000000000000000 ) ) ;
#55152=EDGE_CURVE ( 'NONE', #17076, #43582, #59922, .T. ) ;
#55163=EDGE_LOOP ( 'NONE', ( #83221, #36993, #75389, #81711, #79992 ) ) ;
#55360=LINE ( 'NONE', #21320, #89498 ) ;
#55374=LINE ( 'NONE', #83568, #68204 ) ;
#55376=VERTEX_POINT ( 'NONE', #17081 ) ;
#55444=VERTEX_POINT ( 'NONE', #37962 ) ;
#55465=DIRECTION ( 'NONE',  ( 0.000000000000000000, 0.000000000000000000, -1.000000000000000000 ) ) ;
#55490=DIRECTION ( 'NONE',  ( 0.000000000000000000, -1.000000000000000000, 0.000000000000000000 ) ) ;
#55516=ADVANCED_FACE ( 'NONE', ( #76907 ), #78271, .T. ) ;
#55644=PLANE ( 'NONE',  #78169 ) ;
#55648=CARTESIAN_POINT ( 'NONE',  ( 0.000000000000000000, 127.0000000000000000, 106.1020876358972771 ) ) ;
#55692=CARTESIAN_POINT ( 'NONE',  ( 0.000000000000000000, 239.0000000000000000, 154.6557476874258441 ) ) ;
#55704=ADVANCED_FACE ( 'NONE', ( #76121 ), #88872, .T. ) ;
#55736=EDGE_CURVE ( 'NONE', #4142, #78790, #68865, .T. ) ;
#55774=VECTOR ( 'NONE', #84751, 1000.000000000000000 ) ;
#55931=EDGE_CURVE ( 'NONE', #73188, #48100, #9774, .T. ) ;
#55944=DIRECTION ( 'NONE',  ( 0.000000000000000000, 0.000000000000000000, 1.000000000000000000 ) ) ;
#55945=AXIS2_PLACEMENT_3D ( 'NONE', #78776, #79220, #57856 ) ;
#55961=EDGE_CURVE ( 'NONE', #15070, #28045, #4297, .T. ) ;
#55977=EDGE_CURVE ( 'NONE', #80780, #11707, #37478, .T. ) ;
#56073=ORIENTED_EDGE ( 'NONE', *, *, #55931, .T. ) ;
#56113=ORIENTED_EDGE ( 'NONE', *, *, #37660, .T. ) ;
#56134=EDGE_CURVE ( 'NONE', #78126, #69728, #68760, .T. ) ;
#56195=CONICAL_SURFACE ( 'NONE', #24332, 10.00000000000000888, 0.7853981633974691512 ) ;
#56234=ORIENTED_EDGE ( 'NONE', *, *, #41461, .T. ) ;
#56247=ORIENTED_EDGE ( 'NONE', *, *, #37709, .F. ) ;
#56256=ADVANCED_FACE ( 'NONE', ( #20168, #75580, #13351 ), #46044, .F. ) ;
#56307=DIRECTION ( 'NONE',  ( 1.000000000000000000, -0.000000000000000000, 0.000000000000000000 ) ) ;
#56355=LINE ( 'NONE', #78187, #20776 ) ;
#56411=LINE ( 'NONE', #77324, #47724 ) ;
#56427=ADVANCED_FACE ( 'NONE', ( #30994 ), #78280, .F. ) ;
#56455=CARTESIAN_POINT ( 'NONE',  ( 0.000000000000000000, 238.7999999999999829, 159.6557476874258441 ) ) ;
#56457=DIRECTION ( 'NONE',  ( -1.000000000000000000, 0.000000000000000000, 0.000000000000000000 ) ) ;
#56645=ORIENTED_EDGE ( 'NONE', *, *, #9303, .F. ) ;
#56749=CARTESIAN_POINT ( 'NONE',  ( 1.387778780781445676E-14, 184.0000000000000000, 97.27542076772557778 ) ) ;
#56754=ORIENTED_EDGE ( 'NONE', *, *, #44244, .T. ) ;
#56953=CARTESIAN_POINT ( 'NONE',  ( 89.60916260784479448, 239.0000000000000000, 134.1927865330827103 ) ) ;
#56992=ORIENTED_EDGE ( 'NONE', *, *, #71048, .F. ) ;
#57033=CARTESIAN_POINT ( 'NONE',  ( 1.387778780781445676E-14, 239.0000000000000000, 82.77542076772560620 ) ) ;
#57040=LINE ( 'NONE', #68559, #48780 ) ;
#57080=EDGE_CURVE ( 'NONE', #41873, #83946, #84922, .T. ) ;
#57088=ORIENTED_EDGE ( 'NONE', *, *, #25920, .T. ) ;
#57139=AXIS2_PLACEMENT_3D ( 'NONE', #4892, #61188, #20326 ) ;
#57207=DIRECTION ( 'NONE',  ( 0.000000000000000000, 1.000000000000000000, 0.000000000000000000 ) ) ;
#57332=ORIENTED_EDGE ( 'NONE', *, *, #18188, .F. ) ;
#57354=DIRECTION ( 'NONE',  ( 1.000000000000000000, 0.000000000000000000, -0.000000000000000000 ) ) ;
#57357=DIRECTION ( 'NONE',  ( 0.000000000000000000, 0.000000000000000000, 1.000000000000000000 ) ) ;
#57454=VECTOR ( 'NONE', #67455, 1000.000000000000000 ) ;
#57501=DIRECTION ( 'NONE',  ( 0.000000000000000000, 0.000000000000000000, 1.000000000000000000 ) ) ;
#57504=DIRECTION ( 'NONE',  ( -0.6537961156249243455, 0.7071067811865289210, -0.2693522585644811951 ) ) ;
#57561=DIRECTION ( 'NONE',  ( -0.000000000000000000, 1.000000000000000000, -0.000000000000000000 ) ) ;
#57657=ORIENTED_EDGE ( 'NONE', *, *, #14107, .F. ) ;
#57729=CIRCLE ( 'NONE', #66404, 82.41591158490096802 ) ;
#57824=AXIS2_PLACEMENT_3D ( 'NONE', #81225, #6245, #18972 ) ;
#57856=DIRECTION ( 'NONE',  ( 0.000000000000000000, 0.000000000000000000, -1.000000000000000000 ) ) ;
#57943=DIRECTION ( 'NONE',  ( 0.000000000000000000, 0.000000000000000000, 1.000000000000000000 ) ) ;
#58010=VERTEX_POINT ( 'NONE', #69118 ) ;
#58096=DIRECTION ( 'NONE',  ( 0.000000000000000000, 0.000000000000000000, 1.000000000000000000 ) ) ;
#58127=FILL_AREA_STYLE ('',( #43144 ) ) ;
#58253=DIRECTION ( 'NONE',  ( -1.000000000000000000, 0.000000000000000000, 0.000000000000000000 ) ) ;
#58309=ORIENTED_EDGE ( 'NONE', *, *, #46314, .T. ) ;
#58321=ORIENTED_EDGE ( 'NONE', *, *, #77664, .F. ) ;
#58507=ADVANCED_FACE ( 'NONE', ( #36279 ), #83535, .F. ) ;
#58508=DIRECTION ( 'NONE',  ( 1.000000000000000000, -0.000000000000000000, 0.000000000000000000 ) ) ;
#58523=ORIENTED_EDGE ( 'NONE', *, *, #37615, .F. ) ;
#58623=VECTOR ( 'NONE', #23857, 1000.000000000000000 ) ;
#58674=VECTOR ( 'NONE', #68158, 1000.000000000000000 ) ;
#58683=CARTESIAN_POINT ( 'NONE',  ( -27.27158787008326968, 127.0000000000000000, -0.000000000000000000 ) ) ;
#58732=CARTESIAN_POINT ( 'NONE',  ( 1.473504056721760595E-14, 239.0000000000000000, 104.2754207677255920 ) ) ;
#58743=AXIS2_PLACEMENT_3D ( 'NONE', #14404, #50692, #78433 ) ;
#58779=MECHANICAL_DESIGN_GEOMETRIC_PRESENTATION_REPRESENTATION('',(#3690),#51590);
#58853=AXIS2_PLACEMENT_3D ( 'NONE', #87933, #53823, #38876 ) ;
#58871=ORIENTED_EDGE ( 'NONE', *, *, #67456, .T. ) ;
#59048=CARTESIAN_POINT ( 'NONE',  ( 1.387778780781445676E-14, 223.9999999999999716, 97.27542076772557778 ) ) ;
#59079=LINE ( 'NONE', #4588, #58674 ) ;
#59095=CARTESIAN_POINT ( 'NONE',  ( 0.000000000000000000, 210.0000000000000000, 154.6557476874258441 ) ) ;
#59128=SURFACE_SIDE_STYLE ('',( #51417 ) ) ;
#59241=DIRECTION ( 'NONE',  ( 0.000000000000000000, 0.000000000000000000, -1.000000000000000000 ) ) ;
#59243=CARTESIAN_POINT ( 'NONE',  ( 2.849336855536075284E-14, 184.0000000000000000, 111.9860621927989683 ) ) ;
#59288=CARTESIAN_POINT ( 'NONE',  ( -27.27158787008326968, 184.0000000000000000, 85.23828826961327820 ) ) ;
#59342=ORIENTED_EDGE ( 'NONE', *, *, #77478, .F. ) ;
#59349=LINE ( 'NONE', #3501, #81866 ) ;
#59415=VERTEX_POINT ( 'NONE', #23679 ) ;
#59433=ADVANCED_FACE ( 'NONE', ( #32244 ), #75392, .T. ) ;
#59461=CARTESIAN_POINT ( 'NONE',  ( 2.036081061455522238E-14, 127.0000000000000000, 80.02307622376218887 ) ) ;
#59469=AXIS2_PLACEMENT_3D ( 'NONE', #38351, #24731, #78049 ) ;
#59567=CIRCLE ( 'NONE', #68353, 4.799999999999970512 ) ;
#59753=AXIS2_PLACEMENT_3D ( 'NONE', #27139, #5354, #26239 ) ;
#59763=VECTOR ( 'NONE', #49390, 1000.000000000000000 ) ;
#59775=ORIENTED_EDGE ( 'NONE', *, *, #72403, .F. ) ;
#59789=CARTESIAN_POINT ( 'NONE',  ( 1.387778780781445676E-14, 223.9999999999999716, 97.27542076772557778 ) ) ;
#59853=CONICAL_SURFACE ( 'NONE', #20723, 9.499999999999980460, 0.7853981633974743692 ) ;
#59908=DIRECTION ( 'NONE',  ( 1.000000000000000000, -0.000000000000000000, 0.000000000000000000 ) ) ;
#59922=CIRCLE ( 'NONE', #57139, 7.000000000000006217 ) ;
#59985=DIRECTION ( 'NONE',  ( 0.000000000000000000, 0.000000000000000000, -1.000000000000000000 ) ) ;
#60065=LINE ( 'NONE', #40979, #26999 ) ;
#60152=DIRECTION ( 'NONE',  ( -2.544367396927093358E-16, 0.000000000000000000, -1.000000000000000000 ) ) ;
#60165=EDGE_LOOP ( 'NONE', ( #69640, #28404, #12548, #46730 ) ) ;
#60189=CARTESIAN_POINT ( 'NONE',  ( -89.60916260784479448, 223.9999999999999716, 134.1927865330827103 ) ) ;
#60195=DIRECTION ( 'NONE',  ( 0.000000000000000000, 1.000000000000000000, -0.000000000000000000 ) ) ;
#60372=VECTOR ( 'NONE', #33612, 1000.000000000000000 ) ;
#60396=LINE ( 'NONE', #39960, #72125 ) ;
#60430=ORIENTED_EDGE ( 'NONE', *, *, #24152, .T. ) ;
#60555=ORIENTED_EDGE ( 'NONE', *, *, #37709, .T. ) ;
#60556=DIRECTION ( 'NONE',  ( 2.544367396927093358E-16, -0.000000000000000000, 1.000000000000000000 ) ) ;
#60604=ADVANCED_FACE ( 'NONE', ( #6099 ), #40603, .F. ) ;
#60634=ORIENTED_EDGE ( 'NONE', *, *, #84726, .T. ) ;
#60751=ADVANCED_FACE ( 'NONE', ( #62832 ), #28777, .T. ) ;
#60912=DIRECTION ( 'NONE',  ( -1.000000000000000000, 0.000000000000000000, 0.000000000000000000 ) ) ;
#60914=FACE_OUTER_BOUND ( 'NONE', #54811, .T. ) ;
#61066=ADVANCED_FACE ( 'NONE', ( #27767 ), #11907, .T. ) ;
#61101=ORIENTED_EDGE ( 'NONE', *, *, #13205, .T. ) ;
#61136=CARTESIAN_POINT ( 'NONE',  ( 27.27158787008327678, 184.0000000000000000, 90.32146847885336172 ) ) ;
#61137=ORIENTED_EDGE ( 'NONE', *, *, #71048, .T. ) ;
#61188=DIRECTION ( 'NONE',  ( 0.000000000000000000, 1.000000000000000000, 0.000000000000000000 ) ) ;
#61257=DIRECTION ( 'NONE',  ( 0.000000000000000000, 1.000000000000000000, 0.000000000000000000 ) ) ;
#61362=EDGE_CURVE ( 'NONE', #59415, #77441, #3974, .T. ) ;
#61483=AXIS2_PLACEMENT_3D ( 'NONE', #22393, #1047, #27848 ) ;
#61486=LINE ( 'NONE', #6100, #84083 ) ;
#61501=ORIENTED_EDGE ( 'NONE', *, *, #73675, .F. ) ;
#61503=DIRECTION ( 'NONE',  ( 0.000000000000000000, -0.000000000000000000, 1.000000000000000000 ) ) ;
#61523=CARTESIAN_POINT ( 'NONE',  ( 1.387778780781445676E-14, 223.9999999999999716, 97.27542076772557778 ) ) ;
#61589=EDGE_LOOP ( 'NONE', ( #77310, #58321 ) ) ;
#61752=EDGE_LOOP ( 'NONE', ( #44296, #33418, #18692, #56073 ) ) ;
#61924=CARTESIAN_POINT ( 'NONE',  ( 1.387778780781445676E-14, 239.0000000000000000, 97.27542076772557778 ) ) ;
#61935=DIRECTION ( 'NONE',  ( -0.000000000000000000, -1.000000000000000000, -0.000000000000000000 ) ) ;
#61991=CONICAL_SURFACE ( 'NONE', #83731, 14.49999999999997158, 0.7853981633974743692 ) ;
#62032=AXIS2_PLACEMENT_3D ( 'NONE', #76773, #83159, #89517 ) ;
#62044=CARTESIAN_POINT ( 'NONE',  ( 1.387778780781445676E-14, 224.4999999999999432, 97.27542076772557778 ) ) ;
#62050=ORIENTED_EDGE ( 'NONE', *, *, #14310, .F. ) ;
#62073=AXIS2_PLACEMENT_3D ( 'NONE', #24511, #53058, #46257 ) ;
#62112=CARTESIAN_POINT ( 'NONE',  ( 1.387778780781445676E-14, 223.9999999999999716, 104.4754207677255806 ) ) ;
#62218=FACE_OUTER_BOUND ( 'NONE', #39928, .T. ) ;
#62233=ORIENTED_EDGE ( 'NONE', *, *, #8625, .T. ) ;
#62296=CIRCLE ( 'NONE', #85546, 5.000000000000004441 ) ;
#62449=ORIENTED_EDGE ( 'NONE', *, *, #16071, .F. ) ;
#62493=DIRECTION ( 'NONE',  ( -1.224646799147351482E-16, 0.000000000000000000, -1.000000000000000000 ) ) ;
#62495=ORIENTED_EDGE ( 'NONE', *, *, #89595, .T. ) ;
#62523=AXIS2_PLACEMENT_3D ( 'NONE', #53390, #33428, #18904 ) ;
#62562=LINE ( 'NONE', #62112, #48882 ) ;
#62593=EDGE_CURVE ( 'NONE', #43862, #29586, #89766, .T. ) ;
#62633=DIRECTION ( 'NONE',  ( 0.000000000000000000, 1.000000000000000000, 0.000000000000000000 ) ) ;
#62649=EDGE_LOOP ( 'NONE', ( #51910, #86731, #10520, #19144 ) ) ;
#62690=CARTESIAN_POINT ( 'NONE',  ( 0.000000000000000000, 210.0000000000000000, 145.6557476874258441 ) ) ;
#62696=ORIENTED_EDGE ( 'NONE', *, *, #68308, .F. ) ;
#62819=FILL_AREA_STYLE_COLOUR ( '', #87111 ) ;
#62832=FACE_OUTER_BOUND ( 'NONE', #46967, .T. ) ;
#62889=CARTESIAN_POINT ( 'NONE',  ( 0.000000000000000000, 223.9999999999999716, 154.6557476874258441 ) ) ;
#62919=EDGE_CURVE ( 'NONE', #46976, #21223, #33144, .T. ) ;
#62958=VERTEX_POINT ( 'NONE', #82665 ) ;
#63015=ORIENTED_EDGE ( 'NONE', *, *, #71114, .T. ) ;
#63096=AXIS2_PLACEMENT_3D ( 'NONE', #30036, #50461, #30483 ) ;
#63235=CIRCLE ( 'NONE', #55945, 9.000000000000007105 ) ;
#63243=VECTOR ( 'NONE', #66444, 1000.000000000000000 ) ;
#63245=ORIENTED_EDGE ( 'NONE', *, *, #12060, .T. ) ;
#63253=ORIENTED_EDGE ( 'NONE', *, *, #71496, .F. ) ;
#63426=CIRCLE ( 'NONE', #53201, 5.000000000000004441 ) ;
#63516=CIRCLE ( 'NONE', #41712, 15.00000000000000000 ) ;
#63578=VECTOR ( 'NONE', #68984, 1000.000000000000000 ) ;
#63589=VERTEX_POINT ( 'NONE', #22849 ) ;
#63706=DIRECTION ( 'NONE',  ( -0.000000000000000000, -1.000000000000000000, -0.000000000000000000 ) ) ;
#63720=CARTESIAN_POINT ( 'NONE',  ( 0.000000000000000000, 211.0000000000000000, 154.6557476874258441 ) ) ;
#63891=EDGE_LOOP ( 'NONE', ( #35253, #82757 ) ) ;
#64026=CARTESIAN_POINT ( 'NONE',  ( 1.387778780781445676E-14, 239.0000000000000000, 97.27542076772557778 ) ) ;
#64151=DIRECTION ( 'NONE',  ( 1.000000000000000000, 0.000000000000000000, -0.000000000000000000 ) ) ;
#64172=AXIS2_PLACEMENT_3D ( 'NONE', #53441, #12145, #45733 ) ;
#64272=ORIENTED_EDGE ( 'NONE', *, *, #69619, .T. ) ;
#64296=VECTOR ( 'NONE', #67414, 1000.000000000000000 ) ;
#64335=ORIENTED_EDGE ( 'NONE', *, *, #361, .T. ) ;
#64378=ORIENTED_EDGE ( 'NONE', *, *, #54099, .T. ) ;
#64415=ADVANCED_FACE ( 'NONE', ( #29332 ), #55644, .F. ) ;
#64576=VERTEX_POINT ( 'NONE', #71566 ) ;
#64586=CARTESIAN_POINT ( 'NONE',  ( 0.000000000000000000, 184.0000000000000000, 90.32146847885337593 ) ) ;
#64607=DIRECTION ( 'NONE',  ( 0.000000000000000000, 0.000000000000000000, 1.000000000000000000 ) ) ;
#64610=CARTESIAN_POINT ( 'NONE',  ( 1.475953350320055108E-14, 238.8000000000000114, 90.07542076772557493 ) ) ;
#64639=CIRCLE ( 'NONE', #52988, 14.50000000000001243 ) ;
#64640=EDGE_CURVE ( 'NONE', #64576, #51214, #31540, .T. ) ;
#64681=ORIENTED_EDGE ( 'NONE', *, *, #68176, .T. ) ;
#64694=ORIENTED_EDGE ( 'NONE', *, *, #37517, .F. ) ;
#64740=DIRECTION ( 'NONE',  ( 0.000000000000000000, -1.000000000000000000, 0.000000000000000000 ) ) ;
#64785=EDGE_CURVE ( 'NONE', #20525, #48933, #45489, .T. ) ;
#64808=EDGE_CURVE ( 'NONE', #42743, #79424, #9657, .T. ) ;
#64863=CARTESIAN_POINT ( 'NONE',  ( 0.000000000000000000, 239.0000000000000000, 154.6557476874258441 ) ) ;
#64949=SURFACE_SIDE_STYLE ('',( #16802 ) ) ;
#64973=CARTESIAN_POINT ( 'NONE',  ( -13.40680633928201004, 239.0000000000000000, 102.7987842159323151 ) ) ;
#65014=ORIENTED_EDGE ( 'NONE', *, *, #8041, .F. ) ;
#65026=VECTOR ( 'NONE', #57504, 999.9999999999998863 ) ;
#65068=CARTESIAN_POINT ( 'NONE',  ( -13.86911000615384104, 238.5000000000000000, 102.9892450244911828 ) ) ;
#65105=CARTESIAN_POINT ( 'NONE',  ( -27.27158787008326968, 184.0000000000000000, 0.000000000000000000 ) ) ;
#65156=EDGE_CURVE ( 'NONE', #51214, #21223, #7327, .T. ) ;
#65204=CARTESIAN_POINT ( 'NONE',  ( 27.27158787008328389, 127.0000000000000000, 111.9860621927989683 ) ) ;
#65213=ORIENTED_EDGE ( 'NONE', *, *, #69619, .F. ) ;
#65315=VECTOR ( 'NONE', #59985, 1000.000000000000000 ) ;
#65393=DIRECTION ( 'NONE',  ( 8.881784197001248379E-16, 0.000000000000000000, 1.000000000000000000 ) ) ;
#65561=DIRECTION ( 'NONE',  ( 0.000000000000000000, 0.000000000000000000, 1.000000000000000000 ) ) ;
#65710=ORIENTED_EDGE ( 'NONE', *, *, #34600, .F. ) ;
#65760=EDGE_CURVE ( 'NONE', #45346, #6826, #77951, .T. ) ;
#65780=ORIENTED_EDGE ( 'NONE', *, *, #20074, .F. ) ;
#65854=DIRECTION ( 'NONE',  ( 0.000000000000000000, 1.000000000000000000, -0.000000000000000000 ) ) ;
#65984=ORIENTED_EDGE ( 'NONE', *, *, #13499, .T. ) ;
#66004=DIRECTION ( 'NONE',  ( 2.170915417798913171E-16, 0.000000000000000000, 1.000000000000000000 ) ) ;
#66050=AXIS2_PLACEMENT_3D ( 'NONE', #49641, #77366, #1524 ) ;
#66052=FACE_OUTER_BOUND ( 'NONE', #60165, .T. ) ;
#66071=DIRECTION ( 'NONE',  ( 0.000000000000000000, 0.000000000000000000, 1.000000000000000000 ) ) ;
#66148=DIRECTION ( 'NONE',  ( 0.000000000000000000, 1.000000000000000000, -0.000000000000000000 ) ) ;
#66184=ORIENTED_EDGE ( 'NONE', *, *, #87464, .F. ) ;
#66211=CARTESIAN_POINT ( 'NONE',  ( 0.000000000000000000, 184.0000000000000000, 101.0189074266571794 ) ) ;
#66212=ORIENTED_EDGE ( 'NONE', *, *, #72403, .T. ) ;
#66280=ADVANCED_FACE ( 'NONE', ( #77379 ), #8803, .F. ) ;
#66282=LINE ( 'NONE', #32662, #40350 ) ;
#66295=EDGE_CURVE ( 'NONE', #29586, #17964, #31955, .T. ) ;
#66307=AXIS2_PLACEMENT_3D ( 'NONE', #77050, #78849, #37497 ) ;
#66330=CONICAL_SURFACE ( 'NONE', #86657, 82.41591158490092539, 0.7853981633974760346 ) ;
#66404=AXIS2_PLACEMENT_3D ( 'NONE', #27564, #40732, #13050 ) ;
#66435=VERTEX_POINT ( 'NONE', #71475 ) ;
#66444=DIRECTION ( 'NONE',  ( -0.000000000000000000, -1.000000000000000000, -0.000000000000000000 ) ) ;
#66481=CARTESIAN_POINT ( 'NONE',  ( 2.849336855536075284E-14, 184.0000000000000000, 111.9860621927989683 ) ) ;
#66511=FACE_BOUND ( 'NONE', #61589, .T. ) ;
#66525=LINE ( 'NONE', #4314, #64296 ) ;
#66600=DIRECTION ( 'NONE',  ( -0.000000000000000000, -1.000000000000000000, -0.000000000000000000 ) ) ;
#66736=DIRECTION ( 'NONE',  ( -0.000000000000000000, -1.000000000000000000, -0.000000000000000000 ) ) ;
#66751=DIRECTION ( 'NONE',  ( 0.000000000000000000, 0.000000000000000000, -1.000000000000000000 ) ) ;
#66898=DIRECTION ( 'NONE',  ( 1.365069428641121829E-15, 0.000000000000000000, 1.000000000000000000 ) ) ;
#66914=CARTESIAN_POINT ( 'NONE',  ( -24.79284581386642827, 184.0000000000000000, 0.000000000000000000 ) ) ;
#66959=PLANE ( 'NONE',  #54971 ) ;
#66963=DIRECTION ( 'NONE',  ( 0.000000000000000000, 1.000000000000000000, -0.000000000000000000 ) ) ;
#66971=ORIENTED_EDGE ( 'NONE', *, *, #87, .T. ) ;
#67000=ORIENTED_EDGE ( 'NONE', *, *, #73704, .F. ) ;
#67018=AXIS2_PLACEMENT_3D ( 'NONE', #64863, #71247, #37160 ) ;
#67029=PRODUCT_DEFINITION_SHAPE ( 'NONE', 'NONE',  #3331 ) ;
#67032=AXIS2_PLACEMENT_3D ( 'NONE', #32046, #46998, #19322 ) ;
#67033=ADVANCED_FACE ( 'NONE', ( #73576 ), #11352, .T. ) ;
#67055=VERTEX_POINT ( 'NONE', #77615 ) ;
#67130=CARTESIAN_POINT ( 'NONE',  ( 89.60916260784479448, 239.0000000000000000, 134.1927865330827103 ) ) ;
#67182=ORIENTED_EDGE ( 'NONE', *, *, #50617, .T. ) ;
#67231=ADVANCED_FACE ( 'NONE', ( #52102 ), #71699, .T. ) ;
#67262=CARTESIAN_POINT ( 'NONE',  ( -27.27158787008326968, 184.0000000000000000, 0.000000000000000000 ) ) ;
#67302=ORIENTED_EDGE ( 'NONE', *, *, #14524, .T. ) ;
#67383=LINE ( 'NONE', #18342, #74379 ) ;
#67403=CARTESIAN_POINT ( 'NONE',  ( 0.000000000000000000, 215.0000000000000000, 164.6557476874258441 ) ) ;
#67414=DIRECTION ( 'NONE',  ( -0.000000000000000000, -1.000000000000000000, -0.000000000000000000 ) ) ;
#67455=DIRECTION ( 'NONE',  ( 0.000000000000000000, 1.000000000000000000, 0.000000000000000000 ) ) ;
#67456=EDGE_CURVE ( 'NONE', #24524, #62958, #35162, .T. ) ;
#67497=LINE ( 'NONE', #61136, #18380 ) ;
#67523=CYLINDRICAL_SURFACE ( 'NONE', #21647, 5.000000000000004441 ) ;
#67568=DIRECTION ( 'NONE',  ( -1.000000000000000000, 0.000000000000000000, -0.000000000000000000 ) ) ;
#67573=FACE_OUTER_BOUND ( 'NONE', #46575, .T. ) ;
#67620=EDGE_CURVE ( 'NONE', #6826, #82100, #57729, .T. ) ;
#67658=CARTESIAN_POINT ( 'NONE',  ( -24.79284581386642827, 184.0000000000000000, 90.32146847885337593 ) ) ;
#67775=ORIENTED_EDGE ( 'NONE', *, *, #80565, .F. ) ;
#67787=ORIENTED_EDGE ( 'NONE', *, *, #779, .T. ) ;
#67869=CARTESIAN_POINT ( 'NONE',  ( 0.000000000000000000, 223.9999999999999716, 159.6557476874258441 ) ) ;
#67927=ORIENTED_EDGE ( 'NONE', *, *, #34600, .T. ) ;
#68031=ADVANCED_FACE ( 'NONE', ( #86292 ), #9892, .T. ) ;
#68119=AXIS2_PLACEMENT_3D ( 'NONE', #69314, #34330, #20714 ) ;
#68158=DIRECTION ( 'NONE',  ( -0.000000000000000000, -1.000000000000000000, -0.000000000000000000 ) ) ;
#68176=EDGE_CURVE ( 'NONE', #29586, #43862, #27317, .T. ) ;
#68204=VECTOR ( 'NONE', #20445, 1000.000000000000000 ) ;
#68308=EDGE_CURVE ( 'NONE', #38663, #1545, #8473, .T. ) ;
#68340=CARTESIAN_POINT ( 'NONE',  ( 0.000000000000000000, 223.9999999999999716, 154.6557476874258441 ) ) ;
#68353=AXIS2_PLACEMENT_3D ( 'NONE', #83512, #28082, #68987 ) ;
#68405=LINE ( 'NONE', #35542, #53266 ) ;
#68559=CARTESIAN_POINT ( 'NONE',  ( 13.40680633928208465, 223.9999999999999716, 102.7987842159323151 ) ) ;
#68635=CARTESIAN_POINT ( 'NONE',  ( 0.000000000000000000, 239.0000000000000000, 0.000000000000000000 ) ) ;
#68646=ORIENTED_EDGE ( 'NONE', *, *, #39103, .F. ) ;
#68657=DIRECTION ( 'NONE',  ( 0.000000000000000000, 0.000000000000000000, 1.000000000000000000 ) ) ;
#68672=CIRCLE ( 'NONE', #87545, 5.000000000000004441 ) ;
#68685=CARTESIAN_POINT ( 'NONE',  ( 6.123233995736773185E-16, 215.0000000000000000, 149.6557476874258441 ) ) ;
#68754=DIRECTION ( 'NONE',  ( 0.000000000000000000, 1.000000000000000000, 0.000000000000000000 ) ) ;
#68755=AXIS2_PLACEMENT_3D ( 'NONE', #59789, #89319, #75237 ) ;
#68760=LINE ( 'NONE', #12010, #28219 ) ;
#68828=AXIS2_PLACEMENT_3D ( 'NONE', #13455, #47945, #34333 ) ;
#68865=LINE ( 'NONE', #13901, #81873 ) ;
#68876=DIRECTION ( 'NONE',  ( 0.000000000000000000, 1.000000000000000000, 0.000000000000000000 ) ) ;
#68940=CIRCLE ( 'NONE', #63096, 7.199999999999998401 ) ;
#68978=EDGE_LOOP ( 'NONE', ( #12071, #11417, #52229, #74662 ) ) ;
#68984=DIRECTION ( 'NONE',  ( -0.000000000000000000, -1.000000000000000000, -0.000000000000000000 ) ) ;
#68987=DIRECTION ( 'NONE',  ( 0.000000000000000000, 0.000000000000000000, 1.000000000000000000 ) ) ;
#69010=ORIENTED_EDGE ( 'NONE', *, *, #42823, .T. ) ;
#69118=CARTESIAN_POINT ( 'NONE',  ( 1.475953350320055108E-14, 223.9999999999999716, 104.4754207677255806 ) ) ;
#69196=AXIS2_PLACEMENT_3D ( 'NONE', #82862, #6984, #76021 ) ;
#69244=ORIENTED_EDGE ( 'NONE', *, *, #75040, .F. ) ;
#69314=CARTESIAN_POINT ( 'NONE',  ( 0.000000000000000000, 215.0000000000000000, 154.6557476874258441 ) ) ;
#69394=ORIENTED_EDGE ( 'NONE', *, *, #37162, .T. ) ;
#69403=ORIENTED_EDGE ( 'NONE', *, *, #68308, .T. ) ;
#69473=ORIENTED_EDGE ( 'NONE', *, *, #64785, .F. ) ;
#69554=CARTESIAN_POINT ( 'NONE',  ( -89.60916260784479448, 238.5000000000000000, 134.1927865330827103 ) ) ;
#69556=ORIENTED_EDGE ( 'NONE', *, *, #83386, .F. ) ;
#69577=FACE_OUTER_BOUND ( 'NONE', #18196, .T. ) ;
#69579=VECTOR ( 'NONE', #8918, 1000.000000000000114 ) ;
#69619=EDGE_CURVE ( 'NONE', #10090, #78353, #11152, .T. ) ;
#69640=ORIENTED_EDGE ( 'NONE', *, *, #14319, .F. ) ;
#69728=VERTEX_POINT ( 'NONE', #34281 ) ;
#69743=VECTOR ( 'NONE', #63706, 1000.000000000000000 ) ;
#69763=CYLINDRICAL_SURFACE ( 'NONE', #68119, 5.000000000000004441 ) ;
#69868=CARTESIAN_POINT ( 'NONE',  ( 0.000000000000000000, 224.4999999999999432, 164.6557476874258441 ) ) ;
#69958=DIRECTION ( 'NONE',  ( 0.000000000000000000, -1.000000000000000000, 0.000000000000000000 ) ) ;
#70100=DIRECTION ( 'NONE',  ( -0.000000000000000000, 1.000000000000000000, -0.000000000000000000 ) ) ;
#70367=ORIENTED_EDGE ( 'NONE', *, *, #83337, .T. ) ;
#70479=DIRECTION ( 'NONE',  ( 1.000000000000000000, 0.000000000000000000, 0.000000000000000000 ) ) ;
#70594=EDGE_LOOP ( 'NONE', ( #56113, #88712, #69556, #29715 ) ) ;
#70622=ORIENTED_EDGE ( 'NONE', *, *, #83235, .T. ) ;
#70636=AXIS2_PLACEMENT_3D ( 'NONE', #43276, #56457, #57357 ) ;
#70657=CIRCLE ( 'NONE', #37319, 7.199999999999998401 ) ;
#70679=DIRECTION ( 'NONE',  ( 0.000000000000000000, 0.000000000000000000, 1.000000000000000000 ) ) ;
#70931=ORIENTED_EDGE ( 'NONE', *, *, #62593, .F. ) ;
#70974=DIRECTION ( 'NONE',  ( 1.000000000000000000, 0.000000000000000000, -2.544367396927093851E-16 ) ) ;
#70996=VERTEX_POINT ( 'NONE', #12410 ) ;
#71007=( NAMED_UNIT ( * ) SI_UNIT ( $, .STERADIAN. ) SOLID_ANGLE_UNIT ( ) );
#71048=EDGE_CURVE ( 'NONE', #42743, #10090, #56411, .T. ) ;
#71114=EDGE_CURVE ( 'NONE', #1202, #48691, #85055, .T. ) ;
#71118=LINE ( 'NONE', #2516, #55774 ) ;
#71242=DIRECTION ( 'NONE',  ( 0.000000000000000000, 0.000000000000000000, 1.000000000000000000 ) ) ;
#71247=DIRECTION ( 'NONE',  ( 0.000000000000000000, 1.000000000000000000, -0.000000000000000000 ) ) ;
#71248=VERTEX_POINT ( 'NONE', #16443 ) ;
#71254=ORIENTED_EDGE ( 'NONE', *, *, #55961, .T. ) ;
#71374=DIRECTION ( 'NONE',  ( 0.000000000000000000, 0.000000000000000000, -1.000000000000000000 ) ) ;
#71423=CONICAL_SURFACE ( 'NONE', #27894, 81.91591158490091118, 0.7853981633974760346 ) ;
#71427=ORIENTED_EDGE ( 'NONE', *, *, #44664, .T. ) ;
#71475=CARTESIAN_POINT ( 'NONE',  ( -27.27158787008326968, 184.0000000000000000, 101.0189074266571794 ) ) ;
#71496=EDGE_CURVE ( 'NONE', #83946, #26848, #23131, .T. ) ;
#71566=CARTESIAN_POINT ( 'NONE',  ( 27.27158787008328389, 184.0000000000000000, 111.9860621927989683 ) ) ;
#71598=DIRECTION ( 'NONE',  ( 0.000000000000000000, -1.000000000000000000, 0.000000000000000000 ) ) ;
#71608=DIRECTION ( 'NONE',  ( 0.000000000000000000, 1.000000000000000000, -0.000000000000000000 ) ) ;
#71657=CARTESIAN_POINT ( 'NONE',  ( 27.27158787008325902, 127.0000000000000000, -5.920431057502157584E-15 ) ) ;
#71695=LINE ( 'NONE', #2658, #36393 ) ;
#71699=CYLINDRICAL_SURFACE ( 'NONE', #17737, 7.199999999999998401 ) ;
#71754=AXIS2_PLACEMENT_3D ( 'NONE', #59048, #52223, #79987 ) ;
#71765=DIRECTION ( 'NONE',  ( 0.000000000000000000, 1.000000000000000000, 0.000000000000000000 ) ) ;
#71766=ORIENTED_EDGE ( 'NONE', *, *, #87464, .T. ) ;
#71780=EDGE_CURVE ( 'NONE', #15679, #73188, #34830, .T. ) ;
#71799=APPLICATION_CONTEXT ( 'automotive_design' ) ;
#71806=AXIS2_PLACEMENT_3D ( 'NONE', #39544, #20460, #81797 ) ;
#71900=CARTESIAN_POINT ( 'NONE',  ( 0.000000000000000000, 127.0000000000000000, 90.32146847885336172 ) ) ;
#71901=DIRECTION ( 'NONE',  ( 0.000000000000000000, 0.000000000000000000, -1.000000000000000000 ) ) ;
#71927=LINE ( 'NONE', #85574, #13711 ) ;
#72080=CARTESIAN_POINT ( 'NONE',  ( 0.000000000000000000, 238.5000000000000000, 154.6557476874258441 ) ) ;
#72112=DIRECTION ( 'NONE',  ( -1.000000000000000000, 0.000000000000000000, 2.170915417798913171E-16 ) ) ;
#72125=VECTOR ( 'NONE', #80421, 1000.000000000000000 ) ;
#72130=ORIENTED_EDGE ( 'NONE', *, *, #24152, .F. ) ;
#72224=ORIENTED_EDGE ( 'NONE', *, *, #37615, .T. ) ;
#72293=LINE ( 'NONE', #45004, #8430 ) ;
#72305=CARTESIAN_POINT ( 'NONE',  ( 0.000000000000000000, 184.0000000000000000, 85.23828826961327820 ) ) ;
#72310=CYLINDRICAL_SURFACE ( 'NONE', #34893, 10.00000000000000888 ) ;
#72403=EDGE_CURVE ( 'NONE', #21297, #87703, #44126, .T. ) ;
#72493=DIRECTION ( 'NONE',  ( 0.000000000000000000, 0.000000000000000000, -1.000000000000000000 ) ) ;
#72556=EDGE_CURVE ( 'NONE', #66435, #25689, #3271, .T. ) ;
#72611=ORIENTED_EDGE ( 'NONE', *, *, #76501, .T. ) ;
#72612=ADVANCED_FACE ( 'NONE', ( #17781 ), #72310, .T. ) ;
#72647=CARTESIAN_POINT ( 'NONE',  ( 0.000000000000000000, 224.4999999999999432, 164.6557476874258441 ) ) ;
#72676=VECTOR ( 'NONE', #47069, 1000.000000000000000 ) ;
#72703=AXIS2_PLACEMENT_3D ( 'NONE', #43946, #49864, #71242 ) ;
#72737=EDGE_LOOP ( 'NONE', ( #1397, #19409, #44600, #85248 ) ) ;
#72758=ORIENTED_EDGE ( 'NONE', *, *, #39103, .T. ) ;
#72825=EDGE_CURVE ( 'NONE', #73315, #4973, #84053, .T. ) ;
#72866=DIRECTION ( 'NONE',  ( 0.000000000000000000, 0.000000000000000000, 1.000000000000000000 ) ) ;
#72870=DIRECTION ( 'NONE',  ( 0.000000000000000000, 1.000000000000000000, 0.000000000000000000 ) ) ;
#73023=ORIENTED_EDGE ( 'NONE', *, *, #22766, .F. ) ;
#73106=DIRECTION ( 'NONE',  ( 0.000000000000000000, 1.000000000000000000, 0.000000000000000000 ) ) ;
#73188=VERTEX_POINT ( 'NONE', #14452 ) ;
#73197=VERTEX_POINT ( 'NONE', #21716 ) ;
#73252=CARTESIAN_POINT ( 'NONE',  ( 0.000000000000000000, 238.7999999999999829, 154.6557476874258441 ) ) ;
#73315=VERTEX_POINT ( 'NONE', #49834 ) ;
#73388=ORIENTED_EDGE ( 'NONE', *, *, #76901, .F. ) ;
#73391=CARTESIAN_POINT ( 'NONE',  ( 27.27158787008327678, 184.0000000000000000, 101.0189074266571794 ) ) ;
#73417=DIRECTION ( 'NONE',  ( 0.000000000000000000, 0.000000000000000000, 1.000000000000000000 ) ) ;
#73432=FACE_OUTER_BOUND ( 'NONE', #47636, .T. ) ;
#73507=ADVANCED_FACE ( 'NONE', ( #25717 ), #12095, .T. ) ;
#73512=ORIENTED_EDGE ( 'NONE', *, *, #65156, .F. ) ;
#73548=DIRECTION ( 'NONE',  ( 1.000000000000000000, 0.000000000000000000, -2.544367396927093851E-16 ) ) ;
#73576=FACE_OUTER_BOUND ( 'NONE', #32337, .T. ) ;
#73675=EDGE_CURVE ( 'NONE', #29586, #62958, #48826, .T. ) ;
#73704=EDGE_CURVE ( 'NONE', #11193, #4142, #85817, .T. ) ;
#73753=VERTEX_POINT ( 'NONE', #13885 ) ;
#73859=AXIS2_PLACEMENT_3D ( 'NONE', #2716, #15896, #85843 ) ;
#73865=MECHANICAL_DESIGN_GEOMETRIC_PRESENTATION_REPRESENTATION('',(#8802),#1534);
#74045=ORIENTED_EDGE ( 'NONE', *, *, #55977, .T. ) ;
#74337=CARTESIAN_POINT ( 'NONE',  ( -24.79284581386642827, 127.0000000000000000, 0.000000000000000000 ) ) ;
#74379=VECTOR ( 'NONE', #72870, 1000.000000000000000 ) ;
#74453=CARTESIAN_POINT ( 'NONE',  ( 1.387778780781445676E-14, 238.5000000000000000, 97.27542076772557778 ) ) ;
#74470=CARTESIAN_POINT ( 'NONE',  ( -27.27158787008326968, 127.0000000000000000, 90.32146847885337593 ) ) ;
#74560=EDGE_LOOP ( 'NONE', ( #24253, #33455, #4670, #64694 ) ) ;
#74567=EDGE_CURVE ( 'NONE', #64576, #15070, #29890, .T. ) ;
#74662=ORIENTED_EDGE ( 'NONE', *, *, #34507, .F. ) ;
#74698=ORIENTED_EDGE ( 'NONE', *, *, #64785, .T. ) ;
#74723=ADVANCED_FACE ( 'NONE', ( #24411 ), #45706, .F. ) ;
#74751=COLOUR_RGB ( '', 0.31764706, 0.68627451, 0.89019608) ;
#74788=CARTESIAN_POINT ( 'NONE',  ( 9.261585182541617556, 239.0000000000000000, 152.5407914452011653 ) ) ;
#74990=CLOSED_SHELL ( 'NONE', ( #15845, #49879, #79401, #50732, #31870, #68031, #88147, #39431, #40744, #55704, #20123, #61066, #67231, #25253, #2893, #12640, #67033, #75825, #64415, #83362, #9693, #33506, #74723, #83341, #59433, #14505, #60604, #84259, #27798, #34129, #56427, #73507, #60751, #33062, #40880, #34015, #58507, #18979, #29392, #66280, #56256, #19139, #30823, #89915, #20487, #35956, #38352, #78382, #15673, #6612, #54564, #89803, #43230, #31125, #24643, #72612, #55516, #75248, #77576 ) ) ;
#75040=EDGE_CURVE ( 'NONE', #28033, #78353, #27970, .T. ) ;
#75061=CARTESIAN_POINT ( 'NONE',  ( 0.000000000000000000, 210.0000000000000000, 164.6557476874258441 ) ) ;
#75146=VERTEX_POINT ( 'NONE', #49751 ) ;
#75237=DIRECTION ( 'NONE',  ( 0.000000000000000000, 0.000000000000000000, 1.000000000000000000 ) ) ;
#75248=ADVANCED_FACE ( 'NONE', ( #66511, #80169 ), #44722, .F. ) ;
#75389=ORIENTED_EDGE ( 'NONE', *, *, #24879, .F. ) ;
#75392=PLANE ( 'NONE',  #53004 ) ;
#75408=VECTOR ( 'NONE', #18295, 1000.000000000000000 ) ;
#75413=ORIENTED_EDGE ( 'NONE', *, *, #51140, .T. ) ;
#75554=EDGE_LOOP ( 'NONE', ( #8838, #62449, #79681, #62233 ) ) ;
#75580=FACE_BOUND ( 'NONE', #13871, .T. ) ;
#75589=CARTESIAN_POINT ( 'NONE',  ( -9.261585182541612227, 239.0000000000000000, 152.5407914452011369 ) ) ;
#75724=EDGE_CURVE ( 'NONE', #73753, #41873, #45373, .T. ) ;
#75747=AXIS2_PLACEMENT_3D ( 'NONE', #16156, #64740, #9777 ) ;
#75825=ADVANCED_FACE ( 'NONE', ( #10552 ), #16487, .T. ) ;
#76021=DIRECTION ( 'NONE',  ( 0.000000000000000000, 0.000000000000000000, -1.000000000000000000 ) ) ;
#76062=DIRECTION ( 'NONE',  ( 0.000000000000000000, 0.000000000000000000, 1.000000000000000000 ) ) ;
#76081=ORIENTED_EDGE ( 'NONE', *, *, #40397, .F. ) ;
#76121=FACE_OUTER_BOUND ( 'NONE', #68978, .T. ) ;
#76315=VERTEX_POINT ( 'NONE', #19912 ) ;
#76326=CARTESIAN_POINT ( 'NONE',  ( 6.123233995736769241E-16, 223.9999999999999716, 149.6557476874258441 ) ) ;
#76352=ORIENTED_EDGE ( 'NONE', *, *, #361, .F. ) ;
#76501=EDGE_CURVE ( 'NONE', #9140, #33432, #20810, .T. ) ;
#76505=AXIS2_PLACEMENT_3D ( 'NONE', #44735, #38371, #66071 ) ;
#76773=CARTESIAN_POINT ( 'NONE',  ( 0.000000000000000000, 210.0000000000000000, 154.6557476874258441 ) ) ;
#76869=EDGE_CURVE ( 'NONE', #66435, #42743, #11654, .T. ) ;
#76901=EDGE_CURVE ( 'NONE', #14672, #46763, #26391, .T. ) ;
#76907=FACE_OUTER_BOUND ( 'NONE', #14933, .T. ) ;
#76968=DIRECTION ( 'NONE',  ( 0.000000000000000000, 0.000000000000000000, 1.000000000000000000 ) ) ;
#77038=CARTESIAN_POINT ( 'NONE',  ( 0.000000000000000000, 223.9999999999999716, 154.6557476874258441 ) ) ;
#77050=CARTESIAN_POINT ( 'NONE',  ( 0.000000000000000000, 127.0000000000000000, 0.000000000000000000 ) ) ;
#77052=DIRECTION ( 'NONE',  ( 0.000000000000000000, 0.000000000000000000, 1.000000000000000000 ) ) ;
#77098=EDGE_CURVE ( 'NONE', #73753, #70996, #67383, .T. ) ;
#77126=EDGE_LOOP ( 'NONE', ( #44804, #67182, #88934, #85318 ) ) ;
#77127=DIRECTION ( 'NONE',  ( -2.170915417798913418E-16, 0.000000000000000000, -1.000000000000000000 ) ) ;
#77245=FACE_BOUND ( 'NONE', #5324, .T. ) ;
#77310=ORIENTED_EDGE ( 'NONE', *, *, #52726, .F. ) ;
#77315=LINE ( 'NONE', #15089, #51988 ) ;
#77324=CARTESIAN_POINT ( 'NONE',  ( 0.000000000000000000, 127.0000000000000000, 101.0189074266571794 ) ) ;
#77336=EDGE_LOOP ( 'NONE', ( #11745, #4082, #45630, #79630 ) ) ;
#77366=DIRECTION ( 'NONE',  ( 0.000000000000000000, -1.000000000000000000, 0.000000000000000000 ) ) ;
#77379=FACE_OUTER_BOUND ( 'NONE', #28383, .T. ) ;
#77441=VERTEX_POINT ( 'NONE', #45381 ) ;
#77478=EDGE_CURVE ( 'NONE', #1599, #73197, #38576, .T. ) ;
#77539=ORIENTED_EDGE ( 'NONE', *, *, #32609, .F. ) ;
#77540=ORIENTED_EDGE ( 'NONE', *, *, #87, .F. ) ;
#77576=ADVANCED_FACE ( 'NONE', ( #30885 ), #41026, .T. ) ;
#77615=CARTESIAN_POINT ( 'NONE',  ( 24.79284581386643183, 184.0000000000000000, 90.32146847885336172 ) ) ;
#77664=EDGE_CURVE ( 'NONE', #42594, #9140, #45364, .T. ) ;
#77717=AXIS2_PLACEMENT_3D ( 'NONE', #15457, #9524, #78138 ) ;
#77876=CARTESIAN_POINT ( 'NONE',  ( 0.000000000000000000, 238.5000000000000000, 164.6557476874258441 ) ) ;
#77933=DIRECTION ( 'NONE',  ( 1.000000000000000000, 0.000000000000000000, -1.224646799147353207E-16 ) ) ;
#77951=LINE ( 'NONE', #729, #69579 ) ;
#78044=CARTESIAN_POINT ( 'NONE',  ( 27.27158787008325902, 184.0000000000000000, -5.920431057502157584E-15 ) ) ;
#78049=DIRECTION ( 'NONE',  ( 0.000000000000000000, 0.000000000000000000, -1.000000000000000000 ) ) ;
#78126=VERTEX_POINT ( 'NONE', #74788 ) ;
#78138=DIRECTION ( 'NONE',  ( 0.000000000000000000, 0.000000000000000000, -1.000000000000000000 ) ) ;
#78169=AXIS2_PLACEMENT_3D ( 'NONE', #35226, #83850, #42038 ) ;
#78187=CARTESIAN_POINT ( 'NONE',  ( 24.79284581386643183, 127.0000000000000000, -0.000000000000000000 ) ) ;
#78271=PLANE ( 'NONE',  #61483 ) ;
#78280=PLANE ( 'NONE',  #16640 ) ;
#78347=ORIENTED_EDGE ( 'NONE', *, *, #68176, .F. ) ;
#78353=VERTEX_POINT ( 'NONE', #15259 ) ;
#78382=ADVANCED_FACE ( 'NONE', ( #41146 ), #17887, .T. ) ;
#78415=EDGE_CURVE ( 'NONE', #79965, #33432, #68672, .T. ) ;
#78430=EDGE_LOOP ( 'NONE', ( #14302, #78347, #87886, #62050 ) ) ;
#78433=DIRECTION ( 'NONE',  ( 0.000000000000000000, 0.000000000000000000, 1.000000000000000000 ) ) ;
#78466=ORIENTED_EDGE ( 'NONE', *, *, #22766, .T. ) ;
#78613=VERTEX_POINT ( 'NONE', #4747 ) ;
#78776=CARTESIAN_POINT ( 'NONE',  ( 0.000000000000000000, 210.0000000000000000, 154.6557476874258441 ) ) ;
#78790=VERTEX_POINT ( 'NONE', #56455 ) ;
#78830=DIRECTION ( 'NONE',  ( -0.6537961156249219030, 0.7071067811865322517, 0.2693522585644778089 ) ) ;
#78849=DIRECTION ( 'NONE',  ( 0.000000000000000000, 1.000000000000000000, -0.000000000000000000 ) ) ;
#78875=CARTESIAN_POINT ( 'NONE',  ( 89.60916260784479448, 223.9999999999999716, 134.1927865330827103 ) ) ;
#78903=DIRECTION ( 'NONE',  ( 0.000000000000000000, 0.000000000000000000, 1.000000000000000000 ) ) ;
#79031=LINE ( 'NONE', #29530, #86800 ) ;
#79095=ORIENTED_EDGE ( 'NONE', *, *, #76901, .T. ) ;
#79220=DIRECTION ( 'NONE',  ( 0.000000000000000000, -1.000000000000000000, 0.000000000000000000 ) ) ;
#79270=ORIENTED_EDGE ( 'NONE', *, *, #55736, .F. ) ;
#79332=VECTOR ( 'NONE', #5261, 1000.000000000000000 ) ;
#79401=ADVANCED_FACE ( 'NONE', ( #19053 ), #89156, .T. ) ;
#79412=CARTESIAN_POINT ( 'NONE',  ( 89.60916260784479448, 223.9999999999999716, 134.1927865330827103 ) ) ;
#79424=VERTEX_POINT ( 'NONE', #74470 ) ;
#79480=ORIENTED_EDGE ( 'NONE', *, *, #42823, .F. ) ;
#79611=SHAPE_REPRESENTATION_RELATIONSHIP ( 'NONE' , 'NONE' ,  #19449, #28324 ) ;
#79612=DIRECTION ( 'NONE',  ( 0.000000000000000000, 0.000000000000000000, -1.000000000000000000 ) ) ;
#79630=ORIENTED_EDGE ( 'NONE', *, *, #52956, .T. ) ;
#79681=ORIENTED_EDGE ( 'NONE', *, *, #19324, .F. ) ;
#79794=VERTEX_POINT ( 'NONE', #89233 ) ;
#79799=CIRCLE ( 'NONE', #15992, 15.00000000000000000 ) ;
#79829=LINE ( 'NONE', #74337, #17354 ) ;
#79947=DIRECTION ( 'NONE',  ( 0.000000000000000000, -1.000000000000000000, 0.000000000000000000 ) ) ;
#79965=VERTEX_POINT ( 'NONE', #76326 ) ;
#79987=DIRECTION ( 'NONE',  ( 0.000000000000000000, 0.000000000000000000, 1.000000000000000000 ) ) ;
#79992=ORIENTED_EDGE ( 'NONE', *, *, #46314, .F. ) ;
#80116=CARTESIAN_POINT ( 'NONE',  ( 27.27158787008325902, 184.0000000000000000, -5.920431057502157584E-15 ) ) ;
#80169=FACE_OUTER_BOUND ( 'NONE', #9753, .T. ) ;
#80388=CARTESIAN_POINT ( 'NONE',  ( -24.79284581386642827, 184.0000000000000000, 101.0189074266571794 ) ) ;
#80413=AXIS2_PLACEMENT_3D ( 'NONE', #53174, #25506, #26407 ) ;
#80421=DIRECTION ( 'NONE',  ( 0.000000000000000000, -0.7071067811865321406, -0.7071067811865628938 ) ) ;
#80522=ORIENTED_EDGE ( 'NONE', *, *, #52956, .F. ) ;
#80543=MANIFOLD_SOLID_BREP ( 'Stock-BR-Y-104-1', #74990 ) ;
#80565=EDGE_CURVE ( 'NONE', #80780, #38663, #64639, .T. ) ;
#80610=CARTESIAN_POINT ( 'NONE',  ( 24.79284581386643183, 184.0000000000000000, 101.0189074266571794 ) ) ;
#80637=PLANE ( 'NONE',  #45848 ) ;
#80765=FACE_OUTER_BOUND ( 'NONE', #20689, .T. ) ;
#80780=VERTEX_POINT ( 'NONE', #32194 ) ;
#80978=ORIENTED_EDGE ( 'NONE', *, *, #76869, .F. ) ;
#81008=CARTESIAN_POINT ( 'NONE',  ( 0.000000000000000000, 184.0000000000000000, 90.32146847885336172 ) ) ;
#81056=CIRCLE ( 'NONE', #57824, 5.000000000000004441 ) ;
#81095=LINE ( 'NONE', #33812, #53100 ) ;
#81103=CARTESIAN_POINT ( 'NONE',  ( 0.000000000000000000, 215.0000000000000000, 159.6557476874258441 ) ) ;
#81185=FACE_OUTER_BOUND ( 'NONE', #31414, .T. ) ;
#81225=CARTESIAN_POINT ( 'NONE',  ( 0.000000000000000000, 223.9999999999999716, 154.6557476874258441 ) ) ;
#81256=ORIENTED_EDGE ( 'NONE', *, *, #28557, .F. ) ;
#81347=VECTOR ( 'NONE', #56307, 1000.000000000000000 ) ;
#81384=EDGE_CURVE ( 'NONE', #29549, #4973, #71118, .T. ) ;
#81385=EDGE_LOOP ( 'NONE', ( #46930, #69403, #70367, #32241, #14617 ) ) ;
#81711=ORIENTED_EDGE ( 'NONE', *, *, #56134, .F. ) ;
#81797=DIRECTION ( 'NONE',  ( 1.000000000000000000, 0.000000000000000000, -0.000000000000000000 ) ) ;
#81866=VECTOR ( 'NONE', #31198, 1000.000000000000000 ) ;
#81873=VECTOR ( 'NONE', #6637, 1000.000000000000114 ) ;
#81955=DIRECTION ( 'NONE',  ( -0.000000000000000000, -1.000000000000000000, -0.000000000000000000 ) ) ;
#81983=FACE_OUTER_BOUND ( 'NONE', #85727, .T. ) ;
#82100=VERTEX_POINT ( 'NONE', #75589 ) ;
#82111=CIRCLE ( 'NONE', #5184, 10.00000000000000888 ) ;
#82125=CYLINDRICAL_SURFACE ( 'NONE', #59753, 5.000000000000004441 ) ;
#82152=AXIS2_PLACEMENT_3D ( 'NONE', #52432, #44300, #57943 ) ;
#82172=DIRECTION ( 'NONE',  ( 0.000000000000000000, 0.7071067811865328068, 0.7071067811865622277 ) ) ;
#82240=CARTESIAN_POINT ( 'NONE',  ( 27.27158787008328389, 184.0000000000000000, 106.1020876358972629 ) ) ;
#82245=DIRECTION ( 'NONE',  ( -0.000000000000000000, -1.000000000000000000, -0.000000000000000000 ) ) ;
#82402=FACE_OUTER_BOUND ( 'NONE', #84909, .T. ) ;
#82530=DIRECTION ( 'NONE',  ( -0.000000000000000000, 1.000000000000000000, -0.000000000000000000 ) ) ;
#82588=ORIENTED_EDGE ( 'NONE', *, *, #9303, .T. ) ;
#82637=LINE ( 'NONE', #48955, #63578 ) ;
#82649=ORIENTED_EDGE ( 'NONE', *, *, #65760, .F. ) ;
#82665=CARTESIAN_POINT ( 'NONE',  ( 1.224646799147354440E-15, 215.0000000000000000, 144.6557476874258441 ) ) ;
#82757=ORIENTED_EDGE ( 'NONE', *, *, #27765, .T. ) ;
#82798=CARTESIAN_POINT ( 'NONE',  ( 13.40680633928205268, 239.0000000000000000, 102.7987842159323009 ) ) ;
#82807=CARTESIAN_POINT ( 'NONE',  ( 27.27158787008328389, 127.0000000000000000, 106.1020876358972629 ) ) ;
#82862=CARTESIAN_POINT ( 'NONE',  ( -24.79284581386642827, 184.0000000000000000, 0.000000000000000000 ) ) ;
#82999=ORIENTED_EDGE ( 'NONE', *, *, #3257, .T. ) ;
#83046=EDGE_CURVE ( 'NONE', #38663, #26848, #57040, .T. ) ;
#83091=VECTOR ( 'NONE', #73548, 1000.000000000000000 ) ;
#83112=DIRECTION ( 'NONE',  ( 0.6893610196960207048, -0.7071067811865335839, 0.1574210421884009170 ) ) ;
#83159=DIRECTION ( 'NONE',  ( 0.000000000000000000, -1.000000000000000000, 0.000000000000000000 ) ) ;
#83192=CARTESIAN_POINT ( 'NONE',  ( -27.27158787008326968, 184.0000000000000000, 111.9860621927989826 ) ) ;
#83206=AXIS2_PLACEMENT_3D ( 'NONE', #62044, #49752, #89778 ) ;
#83221=ORIENTED_EDGE ( 'NONE', *, *, #8041, .T. ) ;
#83235=EDGE_CURVE ( 'NONE', #77441, #59415, #31350, .T. ) ;
#83273=LINE ( 'NONE', #27396, #46982 ) ;
#83337=EDGE_CURVE ( 'NONE', #1545, #78613, #8149, .T. ) ;
#83341=ADVANCED_FACE ( 'NONE', ( #81983 ), #80637, .T. ) ;
#83352=DIRECTION ( 'NONE',  ( 0.000000000000000000, 0.000000000000000000, 1.000000000000000000 ) ) ;
#83362=ADVANCED_FACE ( 'NONE', ( #18385 ), #5217, .F. ) ;
#83386=EDGE_CURVE ( 'NONE', #1363, #55007, #81095, .T. ) ;
#83422=AXIS2_PLACEMENT_3D ( 'NONE', #85226, #15273, #77052 ) ;
#83512=CARTESIAN_POINT ( 'NONE',  ( 0.000000000000000000, 239.0000000000000000, 154.6557476874258441 ) ) ;
#83534=DIRECTION ( 'NONE',  ( -1.365069428641121829E-15, 0.000000000000000000, -1.000000000000000000 ) ) ;
#83535=CYLINDRICAL_SURFACE ( 'NONE', #5075, 81.91591158490091118 ) ;
#83568=CARTESIAN_POINT ( 'NONE',  ( 24.79284581386643183, 184.0000000000000000, 90.32146847885336172 ) ) ;
#83570=CARTESIAN_POINT ( 'NONE',  ( 6.123233995736764310E-16, 239.0000000000000000, 149.6557476874258441 ) ) ;
#83731=AXIS2_PLACEMENT_3D ( 'NONE', #64026, #14535, #28136 ) ;
#83794=ORIENTED_EDGE ( 'NONE', *, *, #13588, .T. ) ;
#83842=CIRCLE ( 'NONE', #18594, 10.00000000000000888 ) ;
#83850=DIRECTION ( 'NONE',  ( -1.000000000000000000, 0.000000000000000000, 2.170915417798913171E-16 ) ) ;
#83935=ORIENTED_EDGE ( 'NONE', *, *, #33974, .F. ) ;
#83946=VERTEX_POINT ( 'NONE', #85464 ) ;
#83991=VECTOR ( 'NONE', #58253, 1000.000000000000000 ) ;
#84053=LINE ( 'NONE', #49498, #81347 ) ;
#84083=VECTOR ( 'NONE', #61935, 1000.000000000000000 ) ;
#84097=DIRECTION ( 'NONE',  ( 0.000000000000000000, 0.000000000000000000, 1.000000000000000000 ) ) ;
#84112=CARTESIAN_POINT ( 'NONE',  ( -24.79284581386642827, 184.0000000000000000, 85.23828826961327820 ) ) ;
#84155=DIRECTION ( 'NONE',  ( 1.000000000000000000, -0.000000000000000000, 0.000000000000000000 ) ) ;
#84166=ORIENTED_EDGE ( 'NONE', *, *, #5852, .T. ) ;
#84177=DIRECTION ( 'NONE',  ( 0.000000000000000000, 0.000000000000000000, 1.000000000000000000 ) ) ;
#84214=EDGE_CURVE ( 'NONE', #12137, #55376, #12258, .T. ) ;
#84246=DIRECTION ( 'NONE',  ( -0.000000000000000000, 1.000000000000000000, -0.000000000000000000 ) ) ;
#84259=ADVANCED_FACE ( 'NONE', ( #32696 ), #53103, .T. ) ;
#84267=EDGE_LOOP ( 'NONE', ( #57332, #47077, #60430, #10041 ) ) ;
#84317=CARTESIAN_POINT ( 'NONE',  ( -27.27158787008326968, 184.0000000000000000, 0.000000000000000000 ) ) ;
#84352=ORIENTED_EDGE ( 'NONE', *, *, #37020, .T. ) ;
#84422=FACE_OUTER_BOUND ( 'NONE', #32966, .T. ) ;
#84575=ORIENTED_EDGE ( 'NONE', *, *, #76501, .F. ) ;
#84600=CARTESIAN_POINT ( 'NONE',  ( 0.000000000000000000, 211.0000000000000000, 154.6557476874258441 ) ) ;
#84613=DIRECTION ( 'NONE',  ( -1.000000000000000000, 0.000000000000000000, 0.000000000000000000 ) ) ;
#84726=EDGE_CURVE ( 'NONE', #38527, #15084, #3799, .T. ) ;
#84751=DIRECTION ( 'NONE',  ( 0.000000000000000000, 0.000000000000000000, 1.000000000000000000 ) ) ;
#84844=LINE ( 'NONE', #71657, #9970 ) ;
#84896=ORIENTED_EDGE ( 'NONE', *, *, #25047, .T. ) ;
#84909=EDGE_LOOP ( 'NONE', ( #36257, #51952 ) ) ;
#84922=CIRCLE ( 'NONE', #83422, 10.00000000000000888 ) ;
#84966=SURFACE_STYLE_USAGE ( .BOTH. , #64949 ) ;
#85055=LINE ( 'NONE', #43231, #53542 ) ;
#85057=CARTESIAN_POINT ( 'NONE',  ( 0.000000000000000000, 184.0000000000000000, 85.23828826961327820 ) ) ;
#85071=AXIS2_PLACEMENT_3D ( 'NONE', #68340, #25201, #89238 ) ;
#85088=FILL_AREA_STYLE ('',( #62819 ) ) ;
#85173=ORIENTED_EDGE ( 'NONE', *, *, #3257, .F. ) ;
#85226=CARTESIAN_POINT ( 'NONE',  ( 0.000000000000000000, 224.4999999999999432, 154.6557476874258441 ) ) ;
#85238=CARTESIAN_POINT ( 'NONE',  ( 1.387778780781445676E-14, 238.8000000000000114, 97.27542076772557778 ) ) ;
#85248=ORIENTED_EDGE ( 'NONE', *, *, #35087, .T. ) ;
#85269=DIRECTION ( 'NONE',  ( 0.000000000000000000, 0.000000000000000000, 1.000000000000000000 ) ) ;
#85318=ORIENTED_EDGE ( 'NONE', *, *, #88146, .T. ) ;
#85350=LINE ( 'NONE', #51671, #3665 ) ;
#85464=CARTESIAN_POINT ( 'NONE',  ( 9.749037034254362410, 224.4999999999999432, 152.4294779587682740 ) ) ;
#85501=DIRECTION ( 'NONE',  ( 1.000000000000000000, -0.000000000000000000, 0.000000000000000000 ) ) ;
#85517=CARTESIAN_POINT ( 'NONE',  ( -24.79284581386642827, 184.0000000000000000, 90.32146847885337593 ) ) ;
#85546=AXIS2_PLACEMENT_3D ( 'NONE', #73252, #38293, #65561 ) ;
#85574=CARTESIAN_POINT ( 'NONE',  ( 1.387778780781445676E-14, 239.0000000000000000, 82.77542076772560620 ) ) ;
#85617=EDGE_LOOP ( 'NONE', ( #82649, #40664, #65014, #41790 ) ) ;
#85681=AXIS2_PLACEMENT_3D ( 'NONE', #43738, #6994, #35130 ) ;
#85688=ORIENTED_EDGE ( 'NONE', *, *, #67456, .F. ) ;
#85720=CIRCLE ( 'NONE', #45025, 82.41591158490093960 ) ;
#85727=EDGE_LOOP ( 'NONE', ( #59342, #8270, #63015, #14240 ) ) ;
#85780=VECTOR ( 'NONE', #29130, 1000.000000000000114 ) ;
#85786=DIRECTION ( 'NONE',  ( -0.000000000000000000, -1.000000000000000000, -0.000000000000000000 ) ) ;
#85817=CIRCLE ( 'NONE', #30687, 4.799999999999970512 ) ;
#85843=DIRECTION ( 'NONE',  ( 0.000000000000000000, 0.000000000000000000, 1.000000000000000000 ) ) ;
#85845=CYLINDRICAL_SURFACE ( 'NONE', #2237, 10.00000000000000888 ) ;
#85923=CARTESIAN_POINT ( 'NONE',  ( 0.000000000000000000, 239.0000000000000000, 149.8557476874258896 ) ) ;
#85981=( NAMED_UNIT ( * ) SI_UNIT ( $, .STERADIAN. ) SOLID_ANGLE_UNIT ( ) );
#86012=FACE_OUTER_BOUND ( 'NONE', #55163, .T. ) ;
#86176=ORIENTED_EDGE ( 'NONE', *, *, #87521, .F. ) ;
#86292=FACE_OUTER_BOUND ( 'NONE', #74560, .T. ) ;
#86329=VECTOR ( 'NONE', #47318, 1000.000000000000000 ) ;
#86441=EDGE_CURVE ( 'NONE', #23939, #69728, #19947, .T. ) ;
#86497=ORIENTED_EDGE ( 'NONE', *, *, #42312, .F. ) ;
#86513=CYLINDRICAL_SURFACE ( 'NONE', #20602, 15.00000000000000000 ) ;
#86626=VECTOR ( 'NONE', #54877, 1000.000000000000000 ) ;
#86646=CARTESIAN_POINT ( 'NONE',  ( -27.27158787008326968, 127.0000000000000000, 106.1020876358972771 ) ) ;
#86657=AXIS2_PLACEMENT_3D ( 'NONE', #60189, #46109, #5251 ) ;
#86731=ORIENTED_EDGE ( 'NONE', *, *, #55736, .T. ) ;
#86789=EDGE_LOOP ( 'NONE', ( #64272, #76081, #30003, #62495 ) ) ;
#86800=VECTOR ( 'NONE', #71765, 1000.000000000000000 ) ;
#86836=AXIS2_PLACEMENT_3D ( 'NONE', #6924, #55490, #55944 ) ;
#86839=ORIENTED_EDGE ( 'NONE', *, *, #18188, .T. ) ;
#86866=CARTESIAN_POINT ( 'NONE',  ( -24.79284581386642827, 184.0000000000000000, 0.000000000000000000 ) ) ;
#86914=LINE ( 'NONE', #58732, #47261 ) ;
#86954=CARTESIAN_POINT ( 'NONE',  ( 1.387778780781445676E-14, 223.9999999999999716, 97.27542076772557778 ) ) ;
#87014=DIRECTION ( 'NONE',  ( -0.000000000000000000, 1.000000000000000000, -0.000000000000000000 ) ) ;
#87107=DIRECTION ( 'NONE',  ( 0.000000000000000000, 1.000000000000000000, 0.000000000000000000 ) ) ;
#87111=COLOUR_RGB ( '', 0.31764706, 0.68627451, 0.89019608) ;
#87124=AXIS2_PLACEMENT_3D ( 'NONE', #56749, #22254, #58096 ) ;
#87198=EDGE_LOOP ( 'NONE', ( #87665, #80522, #2065, #69394 ) ) ;
#87366=DIRECTION ( 'NONE',  ( 0.000000000000000000, 0.000000000000000000, 1.000000000000000000 ) ) ;
#87368=EDGE_LOOP ( 'NONE', ( #50964, #53616 ) ) ;
#87389=ORIENTED_EDGE ( 'NONE', *, *, #87471, .F. ) ;
#87441=ORIENTED_EDGE ( 'NONE', *, *, #64808, .F. ) ;
#87464=EDGE_CURVE ( 'NONE', #22883, #77441, #25859, .T. ) ;
#87471=EDGE_CURVE ( 'NONE', #79424, #71248, #66282, .T. ) ;
#87521=EDGE_CURVE ( 'NONE', #83946, #69728, #24522, .T. ) ;
#87545=AXIS2_PLACEMENT_3D ( 'NONE', #77038, #21634, #49306 ) ;
#87583=ORIENTED_EDGE ( 'NONE', *, *, #75724, .T. ) ;
#87626=EDGE_CURVE ( 'NONE', #73315, #28033, #82637, .T. ) ;
#87628=CARTESIAN_POINT ( 'NONE',  ( 0.000000000000000000, 211.0000000000000000, 154.6557476874258441 ) ) ;
#87644=ORIENTED_EDGE ( 'NONE', *, *, #3006, .T. ) ;
#87665=ORIENTED_EDGE ( 'NONE', *, *, #22458, .T. ) ;
#87703=VERTEX_POINT ( 'NONE', #35790 ) ;
#87886=ORIENTED_EDGE ( 'NONE', *, *, #66295, .T. ) ;
#87889=DIRECTION ( 'NONE',  ( -1.000000000000000000, 0.000000000000000000, 2.544367396927093358E-16 ) ) ;
#87897=AXIS2_PLACEMENT_3D ( 'NONE', #55692, #6243, #88918 ) ;
#87913=ORIENTED_EDGE ( 'NONE', *, *, #22014, .F. ) ;
#87933=CARTESIAN_POINT ( 'NONE',  ( 1.387778780781445676E-14, 184.0000000000000000, 97.27542076772557778 ) ) ;
#87999=CYLINDRICAL_SURFACE ( 'NONE', #30608, 81.91591158490091118 ) ;
#88092=DIRECTION ( 'NONE',  ( 0.000000000000000000, 0.000000000000000000, 1.000000000000000000 ) ) ;
#88136=LINE ( 'NONE', #12267, #21160 ) ;
#88146=EDGE_CURVE ( 'NONE', #70996, #45346, #33227, .T. ) ;
#88147=ADVANCED_FACE ( 'NONE', ( #81185 ), #67523, .F. ) ;
#88161=DIRECTION ( 'NONE',  ( 1.694150445170956262E-15, 0.000000000000000000, 1.000000000000000000 ) ) ;
#88190=CIRCLE ( 'NONE', #62032, 9.000000000000007105 ) ;
#88197=CARTESIAN_POINT ( 'NONE',  ( 0.000000000000000000, 239.0000000000000000, 159.6557476874258441 ) ) ;
#88379=DIRECTION ( 'NONE',  ( 0.000000000000000000, 0.000000000000000000, 1.000000000000000000 ) ) ;
#88407=DIRECTION ( 'NONE',  ( -0.000000000000000000, 1.000000000000000000, -0.000000000000000000 ) ) ;
#88464=EDGE_LOOP ( 'NONE', ( #87913, #46884, #72611, #31354 ) ) ;
#88538=ORIENTED_EDGE ( 'NONE', *, *, #62919, .F. ) ;
#88576=DIRECTION ( 'NONE',  ( 0.000000000000000000, 0.000000000000000000, -1.000000000000000000 ) ) ;
#88582=EDGE_CURVE ( 'NONE', #25689, #79424, #61486, .T. ) ;
#88712=ORIENTED_EDGE ( 'NONE', *, *, #35087, .F. ) ;
#88729=AXIS2_PLACEMENT_3D ( 'NONE', #22520, #77933, #62493 ) ;
#88829=VECTOR ( 'NONE', #37783, 1000.000000000000000 ) ;
#88838=CARTESIAN_POINT ( 'NONE',  ( 1.387778780781445676E-14, 239.0000000000000000, 97.27542076772557778 ) ) ;
#88872=CYLINDRICAL_SURFACE ( 'NONE', #68828, 7.199999999999998401 ) ;
#88902=ORIENTED_EDGE ( 'NONE', *, *, #24879, .T. ) ;
#88918=DIRECTION ( 'NONE',  ( 0.000000000000000000, 0.000000000000000000, 1.000000000000000000 ) ) ;
#88934=ORIENTED_EDGE ( 'NONE', *, *, #77098, .T. ) ;
#88979=CARTESIAN_POINT ( 'NONE',  ( 0.000000000000000000, 215.0000000000000000, 154.6557476874258441 ) ) ;
#89080=PLANE ( 'NONE',  #15869 ) ;
#89156=CONICAL_SURFACE ( 'NONE', #36893, 4.799999999999970512, 0.7853981633975198884 ) ;
#89233=CARTESIAN_POINT ( 'NONE',  ( -24.79284581386642827, 127.0000000000000000, 85.23828826961327820 ) ) ;
#89238=DIRECTION ( 'NONE',  ( 0.000000000000000000, 0.000000000000000000, 1.000000000000000000 ) ) ;
#89296=ORIENTED_EDGE ( 'NONE', *, *, #26214, .F. ) ;
#89317=AXIS2_PLACEMENT_3D ( 'NONE', #66211, #3999, #67568 ) ;
#89319=DIRECTION ( 'NONE',  ( 0.000000000000000000, 1.000000000000000000, 0.000000000000000000 ) ) ;
#89331=DIRECTION ( 'NONE',  ( 0.000000000000000000, 0.000000000000000000, 1.000000000000000000 ) ) ;
#89396=LINE ( 'NONE', #27157, #25613 ) ;
#89456=CARTESIAN_POINT ( 'NONE',  ( -89.60916260784479448, 223.9999999999999716, 134.1927865330827103 ) ) ;
#89498=VECTOR ( 'NONE', #83112, 1000.000000000000000 ) ;
#89517=DIRECTION ( 'NONE',  ( 0.000000000000000000, 0.000000000000000000, -1.000000000000000000 ) ) ;
#89595=EDGE_CURVE ( 'NONE', #29549, #10090, #19036, .T. ) ;
#89616=EDGE_CURVE ( 'NONE', #45346, #44762, #79799, .T. ) ;
#89639=VECTOR ( 'NONE', #16646, 1000.000000000000000 ) ;
#89656=CARTESIAN_POINT ( 'NONE',  ( 0.000000000000000000, 0.000000000000000000, 0.000000000000000000 ) ) ;
#89766=CIRCLE ( 'NONE', #31706, 10.00000000000000888 ) ;
#89778=DIRECTION ( 'NONE',  ( 0.000000000000000000, 0.000000000000000000, 1.000000000000000000 ) ) ;
#89803=ADVANCED_FACE ( 'NONE', ( #84422 ), #20336, .T. ) ;
#89915=ADVANCED_FACE ( 'NONE', ( #82402 ), #66959, .T. ) ;
#89917=DIRECTION ( 'NONE',  ( 1.000000000000000000, 0.000000000000000000, -1.365069428641121829E-15 ) ) ;
ENDSEC;
END-ISO-10303-21;
